ISO-10303-21;
HEADER;
FILE_DESCRIPTION (('STEP AP214'),
    '1' );
FILE_NAME ('hex nut gradec_iso_ISO - 4034 - M6 - S.step',
    '2026-10-22T10:02:39',
    ( '' ),
    ( '' ),
    'SwSTEP 2.0',
    'SolidWorks 2026',
    '' );
FILE_SCHEMA (( 'AUTOMOTIVE_DESIGN' ));
ENDSEC;

DATA;
#2=AXIS2_PLACEMENT_3D ( 'NONE', #2206, #5818, #4912 ) ;
#20=APPLICATION_CONTEXT ( 'automotive_design' ) ;
#23=ORIENTED_EDGE ( 'NONE', *, *, #2675, .T. ) ;
#26=CARTESIAN_POINT ( 'NONE',  ( 0.000000000000000000, 5.773502691896260863, -5.653418012614792154 ) ) ;
#37=ORIENTED_EDGE ( 'NONE', *, *, #7774, .F. ) ;
#45=ORIENTED_EDGE ( 'NONE', *, *, #4555, .T. ) ;
#52=VERTEX_POINT ( 'NONE', #2215 ) ;
#56=CARTESIAN_POINT ( 'NONE',  ( 0.000000000000000000, 0.000000000000000000, -6.099999999999999645 ) ) ;
#57=B_SPLINE_CURVE_WITH_KNOTS ( 'NONE', 3,
 ( #11398, #9893, #5467, #4168 ),
 .UNSPECIFIED., .F., .F.,
 ( 4, 4 ),
 ( 2.380735200816727406E-07, 0.002921158011986720298 ),
 .UNSPECIFIED. ) ;
#66=VERTEX_POINT ( 'NONE', #6237 ) ;
#74=ORIENTED_EDGE ( 'NONE', *, *, #10875, .F. ) ;
#75=EDGE_CURVE ( 'NONE', #3733, #9858, #3524, .T. ) ;
#78=DIRECTION ( 'NONE',  ( -1.000000000000000000, 0.000000000000000000, 0.000000000000000000 ) ) ;
#87=DIRECTION ( 'NONE',  ( 1.000000000000000000, 0.000000000000000000, 0.000000000000000000 ) ) ;
#97=DIRECTION ( 'NONE',  ( 0.000000000000000000, -0.000000000000000000, 1.000000000000000000 ) ) ;
#100=CARTESIAN_POINT ( 'NONE',  ( -3.000000000000000000, 0.000000000000000000, -1.753742857142857048 ) ) ;
#103=AXIS2_PLACEMENT_3D ( 'NONE', #3802, #8297, #78 ) ;
#106=ORIENTED_EDGE ( 'NONE', *, *, #10406, .T. ) ;
#113=DIRECTION ( 'NONE',  ( 0.000000000000000000, 0.000000000000000000, 1.000000000000000000 ) ) ;
#123=B_SPLINE_CURVE_WITH_KNOTS ( 'NONE', 3,
 ( #9839, #9954, #7047, #10669, #4339, #2656 ),
 .UNSPECIFIED., .F., .F.,
 ( 4, 2, 4 ),
 ( 0.008070708573309213693, 0.009531758523483282314, 0.01099280847365734920 ),
 .UNSPECIFIED. ) ;
#126=CARTESIAN_POINT ( 'NONE',  ( -5.000000000000000000, 0.000000000000000000, -6.099999999999999645 ) ) ;
#127=AXIS2_PLACEMENT_3D ( 'NONE', #5632, #97, #11119 ) ;
#139=LINE ( 'NONE', #1945, #11400 ) ;
#157=FACE_OUTER_BOUND ( 'NONE', #10390, .T. ) ;
#162=CARTESIAN_POINT ( 'NONE',  ( 0.000000000000000000, 0.000000000000000000, -0.01270000000000047133 ) ) ;
#167=ORIENTED_EDGE ( 'NONE', *, *, #2613, .F. ) ;
#170=ORIENTED_EDGE ( 'NONE', *, *, #3166, .T. ) ;
#175=ADVANCED_FACE ( 'NONE', ( #10161 ), #9210, .T. ) ;
#180=CIRCLE ( 'NONE', #6902, 2.500000000000000000 ) ;
#184=DIRECTION ( 'NONE',  ( 0.000000000000000000, 0.000000000000000000, 1.000000000000000000 ) ) ;
#185=CARTESIAN_POINT ( 'NONE',  ( 0.000000000000000000, 0.000000000000000000, -2.617914285714285416 ) ) ;
#189=EDGE_LOOP ( 'NONE', ( #2988, #1101, #3191 ) ) ;
#190=EDGE_CURVE ( 'NONE', #2213, #10233, #9603, .T. ) ;
#192=DIRECTION ( 'NONE',  ( 0.000000000000000000, 0.000000000000000000, 1.000000000000000000 ) ) ;
#201=CONICAL_SURFACE ( 'NONE', #2897, 2.500000000000000000, 0.9599310885968755924 ) ;
#209=ORIENTED_EDGE ( 'NONE', *, *, #10668, .T. ) ;
#211=CIRCLE ( 'NONE', #6745, 2.500000000000000000 ) ;
#221=DIRECTION ( 'NONE',  ( 0.5000000000000005551, -0.8660254037844383745, 0.000000000000000000 ) ) ;
#222=AXIS2_PLACEMENT_3D ( 'NONE', #671, #2237, #9611 ) ;
#227=DIRECTION ( 'NONE',  ( 0.000000000000000000, 0.000000000000000000, 1.000000000000000000 ) ) ;
#236=EDGE_CURVE ( 'NONE', #9206, #11519, #5249, .T. ) ;
#240=CARTESIAN_POINT ( 'NONE',  ( -2.500000000000000000, 3.061616997868383141E-16, -6.099999999999999645 ) ) ;
#243=FACE_OUTER_BOUND ( 'NONE', #10356, .T. ) ;
#260=CIRCLE ( 'NONE', #1600, 3.000000000000000888 ) ;
#264=CARTESIAN_POINT ( 'NONE',  ( -3.000000000000000000, 0.000000000000000000, -5.210428571428570521 ) ) ;
#265=ORIENTED_EDGE ( 'NONE', *, *, #8549, .F. ) ;
#273=ADVANCED_FACE ( 'NONE', ( #4913 ), #344, .F. ) ;
#281=ORIENTED_EDGE ( 'NONE', *, *, #2765, .F. ) ;
#285=DIRECTION ( 'NONE',  ( -0.8191520442889885789, 1.003171929053520802E-16, 0.5735764363510507113 ) ) ;
#289=CIRCLE ( 'NONE', #9478, 3.000000000000000000 ) ;
#298=EDGE_CURVE ( 'NONE', #1810, #1322, #2665, .T. ) ;
#306=VERTEX_POINT ( 'NONE', #4010 ) ;
#318=CARTESIAN_POINT ( 'NONE',  ( 0.000000000000000000, 0.000000000000000000, -6.099999999999999645 ) ) ;
#323=DIRECTION ( 'NONE',  ( -0.5000000000000006661, 0.8660254037844383745, 0.000000000000000000 ) ) ;
#328=AXIS2_PLACEMENT_3D ( 'NONE', #6832, #8558, #9628 ) ;
#331=CONICAL_SURFACE ( 'NONE', #1858, 3.000000000000000000, 0.9599310885968912466 ) ;
#338=CIRCLE ( 'NONE', #8388, 3.000000000000000000 ) ;
#344=CYLINDRICAL_SURFACE ( 'NONE', #9643, 3.000000000000000888 ) ;
#359=VECTOR ( 'NONE', #9412, 999.9999999999998863 ) ;
#364=VERTEX_POINT ( 'NONE', #1124 ) ;
#368=CONICAL_SURFACE ( 'NONE', #5542, 2.500000000000000000, 0.9599310885968755924 ) ;
#375=ORIENTED_EDGE ( 'NONE', *, *, #453, .F. ) ;
#378=CIRCLE ( 'NONE', #5553, 5.000000000000000888 ) ;
#379=DIRECTION ( 'NONE',  ( 1.000000000000000000, 0.000000000000000000, 0.000000000000000000 ) ) ;
#386=VECTOR ( 'NONE', #9361, 1000.000000000000114 ) ;
#396=ORIENTED_EDGE ( 'NONE', *, *, #10482, .T. ) ;
#398=CARTESIAN_POINT ( 'NONE',  ( -2.450000000000000178, 3.000384657911015863E-16, -0.3851141460153411078 ) ) ;
#406=CARTESIAN_POINT ( 'NONE',  ( 0.000000000000000000, 0.000000000000000000, -1.753742857142857048 ) ) ;
#407=CARTESIAN_POINT ( 'NONE',  ( -1.648146632869006645, -4.821944789745371551, -9.959920860990531005E-16 ) ) ;
#409=DIRECTION ( 'NONE',  ( 0.000000000000000000, 0.000000000000000000, 1.000000000000000000 ) ) ;
#413=VECTOR ( 'NONE', #10435, 1000.000000000000114 ) ;
#429=CARTESIAN_POINT ( 'NONE',  ( 0.000000000000000000, 0.000000000000000000, 0.000000000000000000 ) ) ;
#439=EDGE_CURVE ( 'NONE', #8561, #9242, #6055, .T. ) ;
#444=CARTESIAN_POINT ( 'NONE',  ( -5.000000000000000000, -2.886751345948134428, -0.4465819873852071575 ) ) ;
#445=EDGE_CURVE ( 'NONE', #3923, #1810, #7380, .T. ) ;
#448=ORIENTED_EDGE ( 'NONE', *, *, #1072, .T. ) ;
#453=EDGE_CURVE ( 'NONE', #5713, #10987, #3706, .T. ) ;
#455=ORIENTED_EDGE ( 'NONE', *, *, #1627, .F. ) ;
#498=CARTESIAN_POINT ( 'NONE',  ( 0.000000000000000000, 0.000000000000000000, -2.968018054819144158 ) ) ;
#505=CARTESIAN_POINT ( 'NONE',  ( -2.500000000000000000, 3.061616997868383141E-16, -2.103846626247716234 ) ) ;
#508=CONICAL_SURFACE ( 'NONE', #1852, 3.000000000000000000, 0.9599310885968912466 ) ;
#509=ORIENTED_EDGE ( 'NONE', *, *, #11168, .T. ) ;
#520=DIRECTION ( 'NONE',  ( -1.000000000000000000, 0.000000000000000000, 0.000000000000000000 ) ) ;
#521=CARTESIAN_POINT ( 'NONE',  ( 2.287832656137188447, -4.452621892014644978, -5.917583927755353772E-16 ) ) ;
#534=DIRECTION ( 'NONE',  ( -1.000000000000000000, 0.000000000000000000, 0.000000000000000000 ) ) ;
#535=CONICAL_SURFACE ( 'NONE', #9339, 3.000000000000000000, 0.9599310885968912466 ) ;
#541=VERTEX_POINT ( 'NONE', #1428 ) ;
#551=FACE_OUTER_BOUND ( 'NONE', #562, .T. ) ;
#556=VECTOR ( 'NONE', #11155, 1000.000000000000000 ) ;
#558=ADVANCED_FACE ( 'NONE', ( #7904 ), #1983, .F. ) ;
#562=EDGE_LOOP ( 'NONE', ( #8719, #3480, #10235, #11530 ) ) ;
#570=ADVANCED_FACE ( 'NONE', ( #3399 ), #11717, .F. ) ;
#577=AXIS2_PLACEMENT_3D ( 'NONE', #3496, #11567, #2539 ) ;
#578=DIRECTION ( 'NONE',  ( -0.000000000000000000, -0.000000000000000000, -1.000000000000000000 ) ) ;
#589=EDGE_CURVE ( 'NONE', #6548, #8998, #260, .T. ) ;
#596=CARTESIAN_POINT ( 'NONE',  ( 0.000000000000000000, 0.000000000000000000, -5.560532340533429263 ) ) ;
#597=AXIS2_PLACEMENT_3D ( 'NONE', #6359, #1665, #761 ) ;
#599=AXIS2_PLACEMENT_3D ( 'NONE', #5358, #1631, #1752 ) ;
#602=EDGE_CURVE ( 'NONE', #4836, #8743, #10811, .T. ) ;
#604=B_SPLINE_CURVE_WITH_KNOTS ( 'NONE', 3,
 ( #3860, #10555, #7751, #4149, #4093, #7812, #1399, #3253 ),
 .UNSPECIFIED., .F., .F.,
 ( 4, 2, 2, 4 ),
 ( 0.002921158011986710757, 0.003648658599403066180, 0.004376159186819420302, 0.005831160361652131148 ),
 .UNSPECIFIED. ) ;
#605=EDGE_LOOP ( 'NONE', ( #2787, #4447, #826, #2747 ) ) ;
#608=CARTESIAN_POINT ( 'NONE',  ( -1.653121499799246052, 4.819072548984003390, -0.05140428708382603629 ) ) ;
#609=CYLINDRICAL_SURFACE ( 'NONE', #11207, 2.500000000000000000 ) ;
#613=ORIENTED_EDGE ( 'NONE', *, *, #643, .T. ) ;
#619=EDGE_LOOP ( 'NONE', ( #3574, #9268, #7450, #6908 ) ) ;
#628=LINE ( 'NONE', #2373, #1454 ) ;
#632=CARTESIAN_POINT ( 'NONE',  ( 0.000000000000000000, 0.000000000000000000, -6.099999999999999645 ) ) ;
#643=EDGE_CURVE ( 'NONE', #9312, #7093, #6230, .T. ) ;
#651=DIRECTION ( 'NONE',  ( -0.000000000000000000, -0.000000000000000000, -1.000000000000000000 ) ) ;
#653=CARTESIAN_POINT ( 'NONE',  ( 2.500000000000000000, 0.000000000000000000, -4.696360911962001339 ) ) ;
#663=COLOUR_RGB ( '',1.000000000000000000, 0.9490196078431372140, 0.9098039215686274384 ) ;
#671=CARTESIAN_POINT ( 'NONE',  ( 0.000000000000000000, 0.000000000000000000, -6.099999999999999645 ) ) ;
#695=CARTESIAN_POINT ( 'NONE',  ( 1.443735181952764624, -4.939961795957305668, -0.08165819712377517248 ) ) ;
#710=ADVANCED_FACE ( 'NONE', ( #1827 ), #5856, .F. ) ;
#713=EDGE_LOOP ( 'NONE', ( #11377, #7076, #6758, #8092 ) ) ;
#714=DIRECTION ( 'NONE',  ( 0.000000000000000000, 0.000000000000000000, 1.000000000000000000 ) ) ;
#719=CARTESIAN_POINT ( 'NONE',  ( -3.000000000000000000, 0.000000000000000000, -3.482085714285714229 ) ) ;
#724=DIRECTION ( 'NONE',  ( -0.000000000000000000, -0.000000000000000000, -1.000000000000000000 ) ) ;
#739=CONICAL_SURFACE ( 'NONE', #2475, 3.000000000000000000, 0.9599310885968912466 ) ;
#740=EDGE_LOOP ( 'NONE', ( #1211, #3386, #10270, #4950, #9708, #4672 ) ) ;
#741=EDGE_CURVE ( 'NONE', #11218, #4164, #289, .T. ) ;
#761=DIRECTION ( 'NONE',  ( 0.000000000000000000, 0.000000000000000000, 1.000000000000000000 ) ) ;
#765=CARTESIAN_POINT ( 'NONE',  ( 0.000000000000000000, 0.000000000000000000, -3.131981945180866589 ) ) ;
#776=EDGE_CURVE ( 'NONE', #2110, #3954, #9275, .T. ) ;
#786=CARTESIAN_POINT ( 'NONE',  ( -2.500000000000000000, 3.061616997868383141E-16, -3.131981945180866589 ) ) ;
#789=CIRCLE ( 'NONE', #978, 2.500000000000000000 ) ;
#807=ORIENTED_EDGE ( 'NONE', *, *, #3450, .T. ) ;
#811=CARTESIAN_POINT ( 'NONE',  ( 4.999999999999998224, -2.886751345948137981, -5.653418012614792154 ) ) ;
#813=CARTESIAN_POINT ( 'NONE',  ( 0.000000000000000000, 0.000000000000000000, 0.000000000000000000 ) ) ;
#818=VERTEX_POINT ( 'NONE', #2135 ) ;
#821=EDGE_LOOP ( 'NONE', ( #3246, #9640, #10740, #10037 ) ) ;
#822=DIRECTION ( 'NONE',  ( 0.000000000000000000, 0.000000000000000000, 1.000000000000000000 ) ) ;
#825=CARTESIAN_POINT ( 'NONE',  ( 0.000000000000000000, 0.000000000000000000, -1.753742857142857048 ) ) ;
#826=ORIENTED_EDGE ( 'NONE', *, *, #2571, .T. ) ;
#834=CARTESIAN_POINT ( 'NONE',  ( 4.999999999999998224, -2.886751345948137981, -5.653418012614792154 ) ) ;
#836=EDGE_LOOP ( 'NONE', ( #265, #11815, #613, #5640, #1780, #6974 ) ) ;
#854=ORIENTED_EDGE ( 'NONE', *, *, #8075, .F. ) ;
#858=ORIENTED_EDGE ( 'NONE', *, *, #6456, .F. ) ;
#867=CARTESIAN_POINT ( 'NONE',  ( 0.000000000000000000, 0.000000000000000000, 0.000000000000000000 ) ) ;
#868=CARTESIAN_POINT ( 'NONE',  ( -2.925285743277529438, -4.084588180558409221, -6.089444439476603854 ) ) ;
#900=DIRECTION ( 'NONE',  ( 1.000000000000000000, 0.000000000000000000, 0.000000000000000000 ) ) ;
#903=VECTOR ( 'NONE', #3004, 1000.000000000000000 ) ;
#926=CARTESIAN_POINT ( 'NONE',  ( -5.000000000000000000, -2.886751345948134428, -0.4465819873852071575 ) ) ;
#931=EDGE_CURVE ( 'NONE', #3874, #11822, #10991, .T. ) ;
#933=CARTESIAN_POINT ( 'NONE',  ( 5.000000000000000000, 2.886751345948124214, -6.099999999999999645 ) ) ;
#946=EDGE_CURVE ( 'NONE', #7264, #10278, #57, .T. ) ;
#947=ORIENTED_EDGE ( 'NONE', *, *, #7700, .T. ) ;
#955=AXIS2_PLACEMENT_3D ( 'NONE', #8147, #9335, #10229 ) ;
#964=CARTESIAN_POINT ( 'NONE',  ( 5.000000000000000888, 0.000000000000000000, -6.099999999999999645 ) ) ;
#971=ORIENTED_EDGE ( 'NONE', *, *, #602, .T. ) ;
#972=DIRECTION ( 'NONE',  ( -0.000000000000000000, -0.000000000000000000, -1.000000000000000000 ) ) ;
#973=CARTESIAN_POINT ( 'NONE',  ( 2.500000000000000000, 0.000000000000000000, -3.996153373752295401 ) ) ;
#977=CONICAL_SURFACE ( 'NONE', #8454, 2.500000000000000000, 0.9599310885968755924 ) ;
#978=AXIS2_PLACEMENT_3D ( 'NONE', #596, #3239, #8754 ) ;
#985=ORIENTED_EDGE ( 'NONE', *, *, #11608, .F. ) ;
#991=CARTESIAN_POINT ( 'NONE',  ( 5.000000000000000888, -1.936377641173860908, -0.1973691732449218139 ) ) ;
#993=CARTESIAN_POINT ( 'NONE',  ( 0.000000000000000000, 0.000000000000000000, -4.696360911962001339 ) ) ;
#1000=CARTESIAN_POINT ( 'NONE',  ( 0.000000000000000000, 0.000000000000000000, -1.403639088038009630 ) ) ;
#1010=ORIENTED_EDGE ( 'NONE', *, *, #11325, .T. ) ;
#1017=DIRECTION ( 'NONE',  ( 0.5000000000000009992, 0.8660254037844380415, -0.000000000000000000 ) ) ;
#1032=EDGE_CURVE ( 'NONE', #8985, #10987, #6615, .T. ) ;
#1036=DIRECTION ( 'NONE',  ( 0.000000000000000000, 0.000000000000000000, 1.000000000000000000 ) ) ;
#1040=ORIENTED_EDGE ( 'NONE', *, *, #589, .T. ) ;
#1050=DIRECTION ( 'NONE',  ( -0.000000000000000000, -0.000000000000000000, -1.000000000000000000 ) ) ;
#1053=EDGE_LOOP ( 'NONE', ( #3271, #1726, #7115, #10503 ) ) ;
#1058=DIRECTION ( 'NONE',  ( -1.000000000000000000, 0.000000000000000000, 0.000000000000000000 ) ) ;
#1063=DIRECTION ( 'NONE',  ( -1.000000000000000000, 0.000000000000000000, 0.000000000000000000 ) ) ;
#1064=CARTESIAN_POINT ( 'NONE',  ( -2.500000000000000000, 3.061616997868383141E-16, -5.560532340533429263 ) ) ;
#1072=EDGE_CURVE ( 'NONE', #2315, #4836, #4003, .T. ) ;
#1077=FACE_OUTER_BOUND ( 'NONE', #11804, .T. ) ;
#1081=DIRECTION ( 'NONE',  ( -1.000000000000000000, 0.000000000000000000, 0.000000000000000000 ) ) ;
#1083=AXIS2_PLACEMENT_3D ( 'NONE', #4052, #6635, #3924 ) ;
#1084=DIRECTION ( 'NONE',  ( -0.000000000000000000, -0.000000000000000000, 1.000000000000000000 ) ) ;
#1098=CARTESIAN_POINT ( 'NONE',  ( 0.000000000000000000, 0.000000000000000000, -2.968018054819144158 ) ) ;
#1101=ORIENTED_EDGE ( 'NONE', *, *, #298, .F. ) ;
#1110=EDGE_CURVE ( 'NONE', #5840, #8998, #2890, .T. ) ;
#1111=CARTESIAN_POINT ( 'NONE',  ( 2.500000000000000000, 0.000000000000000000, -3.131981945180866589 ) ) ;
#1112=DIRECTION ( 'NONE',  ( -0.000000000000000000, -0.000000000000000000, -1.000000000000000000 ) ) ;
#1123=FACE_OUTER_BOUND ( 'NONE', #11707, .T. ) ;
#1124=CARTESIAN_POINT ( 'NONE',  ( -2.500000000000005773, -4.330127018922191873, -6.099999999999999645 ) ) ;
#1136=DIRECTION ( 'NONE',  ( 1.000000000000000000, 0.000000000000000000, 0.000000000000000000 ) ) ;
#1147=CARTESIAN_POINT ( 'NONE',  ( -2.500000000000000000, 3.061616997868383141E-16, -3.832189483390572970 ) ) ;
#1148=ORIENTED_EDGE ( 'NONE', *, *, #2304, .F. ) ;
#1150=AXIS2_PLACEMENT_3D ( 'NONE', #7485, #1112, #2137 ) ;
#1157=CARTESIAN_POINT ( 'NONE',  ( 5.000000000000000888, 0.9828435001097619583, -0.04309034703445715347 ) ) ;
#1160=CIRCLE ( 'NONE', #4437, 2.500000000000000000 ) ;
#1161=DIRECTION ( 'NONE',  ( -0.8191520442889974607, 0.000000000000000000, -0.5735764363510379438 ) ) ;
#1163=FACE_OUTER_BOUND ( 'NONE', #7901, .T. ) ;
#1167=ORIENTED_EDGE ( 'NONE', *, *, #4525, .F. ) ;
#1173=CARTESIAN_POINT ( 'NONE',  ( -5.000000000000000000, -0.9724665692850883447, -0.04193043885209645633 ) ) ;
#1185=CARTESIAN_POINT ( 'NONE',  ( 0.000000000000000000, 0.000000000000000000, -1.753742857142857048 ) ) ;
#1189=DIRECTION ( 'NONE',  ( -1.000000000000000000, 0.000000000000000000, 0.000000000000000000 ) ) ;
#1191=EDGE_CURVE ( 'NONE', #1730, #6384, #8567, .T. ) ;
#1200=CARTESIAN_POINT ( 'NONE',  ( 0.000000000000000000, 0.000000000000000000, -2.267810516609437776 ) ) ;
#1211=ORIENTED_EDGE ( 'NONE', *, *, #75, .T. ) ;
#1217=CARTESIAN_POINT ( 'NONE',  ( 4.999999999999999112, 0.4881033300985036516, 4.535861432546776344E-16 ) ) ;
#1221=FACE_OUTER_BOUND ( 'NONE', #11308, .T. ) ;
#1232=ORIENTED_EDGE ( 'NONE', *, *, #946, .F. ) ;
#1241=CARTESIAN_POINT ( 'NONE',  ( -2.500000000000003553, 4.330127018922192761, -6.099999999999999645 ) ) ;
#1247=AXIS2_PLACEMENT_3D ( 'NONE', #5557, #1050, #3815 ) ;
#1253=EDGE_CURVE ( 'NONE', #10987, #5798, #9862, .T. ) ;
#1254=DIRECTION ( 'NONE',  ( -1.000000000000000000, 0.000000000000000000, 0.000000000000000000 ) ) ;
#1256=CARTESIAN_POINT ( 'NONE',  ( 0.000000000000000000, 0.000000000000000000, -6.099999999999999645 ) ) ;
#1265=B_SPLINE_CURVE_WITH_KNOTS ( 'NONE', 3,
 ( #4283, #4224, #11516, #1524, #7886, #1350, #5072, #444 ),
 .UNSPECIFIED., .F., .F.,
 ( 4, 2, 2, 4 ),
 ( 0.002921158011986725936, 0.003648658599403077456, 0.004376159186819428108, 0.005831160361652132015 ),
 .UNSPECIFIED. ) ;
#1268=CIRCLE ( 'NONE', #3564, 2.500000000000000000 ) ;
#1271=LINE ( 'NONE', #4940, #1848 ) ;
#1300=AXIS2_PLACEMENT_3D ( 'NONE', #7858, #10536, #10591 ) ;
#1308=EDGE_CURVE ( 'NONE', #1419, #6608, #6316, .T. ) ;
#1316=EDGE_CURVE ( 'NONE', #1730, #5840, #4967, .T. ) ;
#1322=VERTEX_POINT ( 'NONE', #11595 ) ;
#1325=AXIS2_PLACEMENT_3D ( 'NONE', #1490, #2447, #7907 ) ;
#1333=ADVANCED_FACE ( 'NONE', ( #8020 ), #5928, .F. ) ;
#1348=CARTESIAN_POINT ( 'NONE',  ( 0.000000000000000000, 0.000000000000000000, -6.099999999999999645 ) ) ;
#1349=ORIENTED_EDGE ( 'NONE', *, *, #4258, .F. ) ;
#1350=CARTESIAN_POINT ( 'NONE',  ( -4.180704885107416224, -3.359771601077114589, -0.1983443223721613746 ) ) ;
#1351=CIRCLE ( 'NONE', #1733, 5.000000000000000888 ) ;
#1353=ORIENTED_EDGE ( 'NONE', *, *, #1402, .T. ) ;
#1365=FACE_OUTER_BOUND ( 'NONE', #11648, .T. ) ;
#1372=CARTESIAN_POINT ( 'NONE',  ( 0.000000000000000000, 0.000000000000000000, -1.753742857142857048 ) ) ;
#1378=AXIS2_PLACEMENT_3D ( 'NONE', #4847, #221, #3884 ) ;
#1383=DIRECTION ( 'NONE',  ( 1.000000000000000000, 0.000000000000000000, 0.000000000000000000 ) ) ;
#1386=CARTESIAN_POINT ( 'NONE',  ( -0.8179331680533127313, -5.301268757141564869, -5.926062401966621707 ) ) ;
#1399=CARTESIAN_POINT ( 'NONE',  ( -0.4079457818577089112, 5.537975084925939484, -5.789399939901066716 ) ) ;
#1402=EDGE_CURVE ( 'NONE', #6890, #9107, #1544, .T. ) ;
#1406=DIRECTION ( 'NONE',  ( 0.000000000000000000, 0.000000000000000000, 1.000000000000000000 ) ) ;
#1409=CARTESIAN_POINT ( 'NONE',  ( 2.981862520314375153, 0.000000000000000000, -0.01270000000000047133 ) ) ;
#1419=VERTEX_POINT ( 'NONE', #3468 ) ;
#1422=( NAMED_UNIT ( * ) PLANE_ANGLE_UNIT ( ) SI_UNIT ( $, .RADIAN. ) );
#1428=CARTESIAN_POINT ( 'NONE',  ( -2.500000000000003553, 4.330127018922192761, 0.000000000000000000 ) ) ;
#1430=ADVANCED_FACE ( 'NONE', ( #7134 ), #4393, .F. ) ;
#1435=DIRECTION ( 'NONE',  ( -1.000000000000000000, 0.000000000000000000, 0.000000000000000000 ) ) ;
#1439=CARTESIAN_POINT ( 'NONE',  ( -1.648146632869007089, -4.821944789745371551, -6.099999999999998757 ) ) ;
#1446=ADVANCED_FACE ( 'NONE', ( #10935 ), #10312, .T. ) ;
#1452=CARTESIAN_POINT ( 'NONE',  ( -4.182066831946700702, 3.358985280702823317, -5.926062401966626147 ) ) ;
#1454=VECTOR ( 'NONE', #1644, 1000.000000000000000 ) ;
#1462=AXIS2_PLACEMENT_3D ( 'NONE', #6148, #7884, #6269 ) ;
#1488=DIRECTION ( 'NONE',  ( -0.000000000000000000, -0.000000000000000000, -1.000000000000000000 ) ) ;
#1490=CARTESIAN_POINT ( 'NONE',  ( 0.000000000000000000, 0.000000000000000000, -0.3851141460153411078 ) ) ;
#1499=CARTESIAN_POINT ( 'NONE',  ( -2.500000000000005773, -4.330127018922191873, -6.099999999999999645 ) ) ;
#1504=EDGE_LOOP ( 'NONE', ( #9141, #37, #8640, #10332 ) ) ;
#1505=FACE_OUTER_BOUND ( 'NONE', #8291, .T. ) ;
#1507=VERTEX_POINT ( 'NONE', #8306 ) ;
#1515=ADVANCED_FACE ( 'NONE', ( #3579 ), #5944, .F. ) ;
#1517=LINE ( 'NONE', #8835, #413 ) ;
#1519=VECTOR ( 'NONE', #8861, 1000.000000000000114 ) ;
#1520=FILL_AREA_STYLE_COLOUR ( '', #663 ) ;
#1522=CARTESIAN_POINT ( 'NONE',  ( 0.000000000000000000, 0.000000000000000000, -1.239675197676287643 ) ) ;
#1524=CARTESIAN_POINT ( 'NONE',  ( -3.346878500200761053, -3.841181488860384796, -0.05140428708383018575 ) ) ;
#1535=VECTOR ( 'NONE', #192, 1000.000000000000000 ) ;
#1543=CARTESIAN_POINT ( 'NONE',  ( -1.734723475976807094E-14, -5.773502691896260863, -0.4465819873852071575 ) ) ;
#1544=LINE ( 'NONE', #5211, #1519 ) ;
#1563=AXIS2_PLACEMENT_3D ( 'NONE', #2359, #3142, #7048 ) ;
#1566=DIRECTION ( 'NONE',  ( -0.000000000000000000, -0.000000000000000000, -1.000000000000000000 ) ) ;
#1569=CARTESIAN_POINT ( 'NONE',  ( -3.000000000000000000, 0.000000000000000000, -4.346257142857142597 ) ) ;
#1573=CARTESIAN_POINT ( 'NONE',  ( 5.000000000000000888, 0.9828435001097617363, -6.056909652965543067 ) ) ;
#1574=ORIENTED_EDGE ( 'NONE', *, *, #741, .F. ) ;
#1583=ORIENTED_EDGE ( 'NONE', *, *, #1316, .T. ) ;
#1587=ORIENTED_EDGE ( 'NONE', *, *, #5073, .T. ) ;
#1591=DIRECTION ( 'NONE',  ( 0.000000000000000000, 0.000000000000000000, -1.000000000000000000 ) ) ;
#1598=CARTESIAN_POINT ( 'NONE',  ( 2.074714256722481220, -4.575665857285988736, -0.01055556052339421194 ) ) ;
#1600=AXIS2_PLACEMENT_3D ( 'NONE', #6174, #4367, #8018 ) ;
#1607=ORIENTED_EDGE ( 'NONE', *, *, #9016, .F. ) ;
#1610=EDGE_CURVE ( 'NONE', #1730, #6548, #1829, .T. ) ;
#1613=CARTESIAN_POINT ( 'NONE',  ( 4.592054218142289201, 3.122278952918446038, -5.789399939901072933 ) ) ;
#1621=CARTESIAN_POINT ( 'NONE',  ( -7.511572993685809947E-16, -5.773502691896268857, -6.099999999999999645 ) ) ;
#1627=EDGE_CURVE ( 'NONE', #306, #8424, #2291, .T. ) ;
#1631=DIRECTION ( 'NONE',  ( 0.000000000000000000, -0.000000000000000000, 1.000000000000000000 ) ) ;
#1634=EDGE_LOOP ( 'NONE', ( #5518, #10881, #4927 ) ) ;
#1638=ORIENTED_EDGE ( 'NONE', *, *, #9937, .T. ) ;
#1641=VECTOR ( 'NONE', #9613, 1000.000000000000000 ) ;
#1642=ORIENTED_EDGE ( 'NONE', *, *, #1110, .F. ) ;
#1644=DIRECTION ( 'NONE',  ( 0.8191520442889911324, 0.000000000000000000, 0.5735764363510470476 ) ) ;
#1645=VECTOR ( 'NONE', #5602, 1000.000000000000000 ) ;
#1655=CARTESIAN_POINT ( 'NONE',  ( -2.500000000000000000, 3.061616997868383141E-16, -6.099999999999999645 ) ) ;
#1656=VECTOR ( 'NONE', #285, 1000.000000000000000 ) ;
#1658=CARTESIAN_POINT ( 'NONE',  ( 3.000000000000000888, 3.673940397442060854E-16, -6.074599999999999334 ) ) ;
#1659=VERTEX_POINT ( 'NONE', #3696 ) ;
#1664=VERTEX_POINT ( 'NONE', #1111 ) ;
#1665=DIRECTION ( 'NONE',  ( -1.000000000000000000, 0.000000000000000000, 0.000000000000000000 ) ) ;
#1684=EDGE_CURVE ( 'NONE', #5713, #1761, #6587, .T. ) ;
#1690=B_SPLINE_CURVE_WITH_KNOTS ( 'NONE', 3,
 ( #6658, #6541, #11178, #2934 ),
 .UNSPECIFIED., .F., .F.,
 ( 4, 4 ),
 ( 2.380735200829041942E-07, 0.002921158011986710757 ),
 .UNSPECIFIED. ) ;
#1694=CYLINDRICAL_SURFACE ( 'NONE', #8455, 2.500000000000000000 ) ;
#1718=B_SPLINE_CURVE_WITH_KNOTS ( 'NONE', 3,
 ( #9763, #3242, #4139, #9650 ),
 .UNSPECIFIED., .F., .F.,
 ( 4, 4 ),
 ( 2.380735200850890892E-07, 0.002921158011986708155 ),
 .UNSPECIFIED. ) ;
#1720=CARTESIAN_POINT ( 'NONE',  ( 0.000000000000000000, 0.000000000000000000, -5.724496230895143256 ) ) ;
#1721=CARTESIAN_POINT ( 'NONE',  ( 2.500000000000000000, 0.000000000000000000, -5.560532340533429263 ) ) ;
#1726=ORIENTED_EDGE ( 'NONE', *, *, #10309, .T. ) ;
#1728=AXIS2_PLACEMENT_3D ( 'NONE', #11510, #9719, #5357 ) ;
#1730=VERTEX_POINT ( 'NONE', #5989 ) ;
#1732=DIRECTION ( 'NONE',  ( -1.000000000000000000, 0.000000000000000000, 0.000000000000000000 ) ) ;
#1733=AXIS2_PLACEMENT_3D ( 'NONE', #11841, #4666, #2755 ) ;
#1745=CARTESIAN_POINT ( 'NONE',  ( 2.500000000000005773, 4.330127018922190985, 0.000000000000000000 ) ) ;
#1752=DIRECTION ( 'NONE',  ( -1.000000000000000000, 3.552713678800500929E-15, 0.000000000000000000 ) ) ;
#1761=VERTEX_POINT ( 'NONE', #10395 ) ;
#1766=B_SPLINE_CURVE_WITH_KNOTS ( 'NONE', 3,
 ( #126, #3791, #7460, #2898, #6566, #10195 ),
 .UNSPECIFIED., .F., .F.,
 ( 4, 2, 4 ),
 ( 0.008070708573309213693, 0.009531758523483285783, 0.01099280847365735614 ),
 .UNSPECIFIED. ) ;
#1775=LINE ( 'NONE', #10873, #8415 ) ;
#1780=ORIENTED_EDGE ( 'NONE', *, *, #7542, .T. ) ;
#1783=ORIENTED_EDGE ( 'NONE', *, *, #9045, .T. ) ;
#1784=ADVANCED_FACE ( 'NONE', ( #2313 ), #368, .F. ) ;
#1786=CARTESIAN_POINT ( 'NONE',  ( 0.000000000000000000, 0.000000000000000000, 0.000000000000000000 ) ) ;
#1801=CARTESIAN_POINT ( 'NONE',  ( 0.000000000000000000, 0.000000000000000000, -6.099999999999999645 ) ) ;
#1810=VERTEX_POINT ( 'NONE', #4063 ) ;
#1821=VECTOR ( 'NONE', #2498, 1000.000000000000114 ) ;
#1827=FACE_OUTER_BOUND ( 'NONE', #3118, .T. ) ;
#1829=LINE ( 'NONE', #7306, #10505 ) ;
#1836=DIRECTION ( 'NONE',  ( -1.000000000000000000, 0.000000000000000000, 0.000000000000000000 ) ) ;
#1838=EDGE_CURVE ( 'NONE', #8743, #818, #1897, .T. ) ;
#1847=ORIENTED_EDGE ( 'NONE', *, *, #9016, .T. ) ;
#1848=VECTOR ( 'NONE', #8597, 1000.000000000000000 ) ;
#1852=AXIS2_PLACEMENT_3D ( 'NONE', #2150, #8566, #3835 ) ;
#1858=AXIS2_PLACEMENT_3D ( 'NONE', #4634, #7112, #10914 ) ;
#1862=DIRECTION ( 'NONE',  ( 1.000000000000000000, 0.000000000000000000, 0.000000000000000000 ) ) ;
#1863=APPLICATION_CONTEXT ( 'automotive_design' ) ;
#1887=CARTESIAN_POINT ( 'NONE',  ( -5.000000000000000000, -2.417244626924487605, -0.3110470720778656939 ) ) ;
#1897=CIRCLE ( 'NONE', #11650, 2.500000000000000000 ) ;
#1903=EDGE_CURVE ( 'NONE', #1507, #3923, #11671, .T. ) ;
#1907=DIRECTION ( 'NONE',  ( -1.000000000000000000, 0.000000000000000000, 0.000000000000000000 ) ) ;
#1925=AXIS2_PLACEMENT_3D ( 'NONE', #406, #4973, #9270 ) ;
#1929=CIRCLE ( 'NONE', #8641, 2.500000000000000000 ) ;
#1931=EDGE_LOOP ( 'NONE', ( #5144, #6420, #8047, #4868 ) ) ;
#1940=FACE_OUTER_BOUND ( 'NONE', #4242, .T. ) ;
#1945=CARTESIAN_POINT ( 'NONE',  ( 2.500000000000000000, 0.000000000000000000, -6.099999999999999645 ) ) ;
#1952=DIRECTION ( 'NONE',  ( 0.000000000000000000, 0.000000000000000000, -1.000000000000000000 ) ) ;
#1955=VERTEX_POINT ( 'NONE', #7498 ) ;
#1965=DIRECTION ( 'NONE',  ( 0.000000000000000000, 0.000000000000000000, 1.000000000000000000 ) ) ;
#1972=ORIENTED_EDGE ( 'NONE', *, *, #6412, .T. ) ;
#1976=CARTESIAN_POINT ( 'NONE',  ( 0.000000000000000000, 0.000000000000000000, -6.099999999999999645 ) ) ;
#1983=CONICAL_SURFACE ( 'NONE', #5441, 3.000000000000000000, 0.9599310885968912466 ) ;
#1989=ADVANCED_FACE ( 'NONE', ( #8205 ), #4601, .T. ) ;
#1990=ORIENTED_EDGE ( 'NONE', *, *, #7700, .F. ) ;
#2001=DIRECTION ( 'NONE',  ( 0.000000000000000000, 0.000000000000000000, 1.000000000000000000 ) ) ;
#2010=DIRECTION ( 'NONE',  ( 0.8191520442889885789, 0.000000000000000000, 0.5735764363510507113 ) ) ;
#2024=EDGE_CURVE ( 'NONE', #364, #8530, #1351, .T. ) ;
#2033=EDGE_CURVE ( 'NONE', #10958, #2110, #4494, .T. ) ;
#2034=CARTESIAN_POINT ( 'NONE',  ( 0.000000000000000000, 0.000000000000000000, -6.099999999999999645 ) ) ;
#2048=CIRCLE ( 'NONE', #328, 3.000000000000000000 ) ;
#2049=LINE ( 'NONE', #3728, #1645 ) ;
#2052=CARTESIAN_POINT ( 'NONE',  ( -5.000000000000000888, -1.936377641173858688, -5.902630826755077109 ) ) ;
#2063=DIRECTION ( 'NONE',  ( 1.000000000000000000, 0.000000000000000000, 0.000000000000000000 ) ) ;
#2081=VECTOR ( 'NONE', #10977, 1000.000000000000000 ) ;
#2082=ORIENTED_EDGE ( 'NONE', *, *, #3680, .F. ) ;
#2110=VERTEX_POINT ( 'NONE', #264 ) ;
#2111=FACE_OUTER_BOUND ( 'NONE', #8407, .T. ) ;
#2116=CIRCLE ( 'NONE', #3470, 2.981862520314375153 ) ;
#2118=DIRECTION ( 'NONE',  ( -1.000000000000000000, 0.000000000000000000, 0.000000000000000000 ) ) ;
#2129=ORIENTED_EDGE ( 'NONE', *, *, #10157, .F. ) ;
#2131=AXIS2_PLACEMENT_3D ( 'NONE', #3234, #4132, #5275 ) ;
#2135=CARTESIAN_POINT ( 'NONE',  ( 2.500000000000000000, 0.000000000000000000, -3.832189483390572970 ) ) ;
#2137=DIRECTION ( 'NONE',  ( -1.000000000000000000, 0.000000000000000000, 0.000000000000000000 ) ) ;
#2141=DIRECTION ( 'NONE',  ( -0.8191520442889911324, 1.003171929053523884E-16, 0.5735764363510470476 ) ) ;
#2150=CARTESIAN_POINT ( 'NONE',  ( 0.000000000000000000, 0.000000000000000000, -0.8895714285714284575 ) ) ;
#2166=ORIENTED_EDGE ( 'NONE', *, *, #9821, .T. ) ;
#2170=ORIENTED_EDGE ( 'NONE', *, *, #11241, .F. ) ;
#2172=DIRECTION ( 'NONE',  ( 1.000000000000000000, 0.000000000000000000, 0.000000000000000000 ) ) ;
#2180=FACE_OUTER_BOUND ( 'NONE', #9854, .T. ) ;
#2181=ORIENTED_EDGE ( 'NONE', *, *, #4441, .F. ) ;
#2206=CARTESIAN_POINT ( 'NONE',  ( 0.000000000000000000, 0.000000000000000000, -4.346257142857142597 ) ) ;
#2212=EDGE_CURVE ( 'NONE', #10278, #11839, #4197, .T. ) ;
#2213=VERTEX_POINT ( 'NONE', #3503 ) ;
#2215=CARTESIAN_POINT ( 'NONE',  ( 3.000000000000000888, 0.000000000000000000, -6.099999999999997868 ) ) ;
#2221=ORIENTED_EDGE ( 'NONE', *, *, #8514, .F. ) ;
#2230=CARTESIAN_POINT ( 'NONE',  ( 0.000000000000000000, 0.000000000000000000, -5.560532340533429263 ) ) ;
#2237=DIRECTION ( 'NONE',  ( -0.000000000000000000, -0.000000000000000000, 1.000000000000000000 ) ) ;
#2239=CONICAL_SURFACE ( 'NONE', #3974, 2.500000000000000000, 0.9599310885968755924 ) ;
#2241=ORIENTED_EDGE ( 'NONE', *, *, #6430, .T. ) ;
#2243=CARTESIAN_POINT ( 'NONE',  ( -2.074714256722480776, 4.575665857285978966, -0.01055556052338894012 ) ) ;
#2252=ORIENTED_EDGE ( 'NONE', *, *, #10689, .T. ) ;
#2257=AXIS2_PLACEMENT_3D ( 'NONE', #1256, #2948, #3845 ) ;
#2285=DIRECTION ( 'NONE',  ( -1.000000000000000000, 0.000000000000000000, 0.000000000000000000 ) ) ;
#2291=CIRCLE ( 'NONE', #8992, 2.500000000000000000 ) ;
#2292=DIRECTION ( 'NONE',  ( 1.000000000000000000, 0.000000000000000000, 0.000000000000000000 ) ) ;
#2301=CARTESIAN_POINT ( 'NONE',  ( -3.000000000000000000, 0.000000000000000000, -5.210428571428570521 ) ) ;
#2304=EDGE_CURVE ( 'NONE', #4836, #4164, #7465, .T. ) ;
#2312=CIRCLE ( 'NONE', #9012, 2.500000000000000000 ) ;
#2313=FACE_OUTER_BOUND ( 'NONE', #619, .T. ) ;
#2315=VERTEX_POINT ( 'NONE', #973 ) ;
#2320=AXIS2_PLACEMENT_3D ( 'NONE', #318, #8416, #10383 ) ;
#2321=AXIS2_PLACEMENT_3D ( 'NONE', #2034, #3002, #9345 ) ;
#2322=CARTESIAN_POINT ( 'NONE',  ( 3.000000000000000000, 3.673940397442059868E-16, -1.753742857142857048 ) ) ;
#2324=EDGE_LOOP ( 'NONE', ( #8002, #10768, #10576, #6663 ) ) ;
#2336=DIRECTION ( 'NONE',  ( -0.000000000000000000, -0.000000000000000000, 1.000000000000000000 ) ) ;
#2337=CONICAL_SURFACE ( 'NONE', #4060, 2.450000000000000178, 0.9599310885968801443 ) ;
#2351=CARTESIAN_POINT ( 'NONE',  ( 0.000000000000000000, 0.000000000000000000, -2.968018054819144158 ) ) ;
#2359=CARTESIAN_POINT ( 'NONE',  ( 0.000000000000000000, 0.000000000000000000, 0.000000000000000000 ) ) ;
#2373=CARTESIAN_POINT ( 'NONE',  ( 2.450000000000000178, 0.000000000000000000, -0.3851141460153411078 ) ) ;
#2374=VECTOR ( 'NONE', #5323, 1000.000000000000000 ) ;
#2380=CARTESIAN_POINT ( 'NONE',  ( 0.000000000000000000, 0.000000000000000000, -2.103846626247716234 ) ) ;
#2382=DIRECTION ( 'NONE',  ( 0.8191520442889885789, 0.000000000000000000, 0.5735764363510507113 ) ) ;
#2395=AXIS2_PLACEMENT_3D ( 'NONE', #7305, #1952, #9203 ) ;
#2411=CONICAL_SURFACE ( 'NONE', #10624, 2.500000000000000000, 0.9599310885968755924 ) ;
#2422=ORIENTED_EDGE ( 'NONE', *, *, #9932, .F. ) ;
#2426=EDGE_CURVE ( 'NONE', #5005, #7264, #6502, .T. ) ;
#2427=ORIENTED_EDGE ( 'NONE', *, *, #2426, .T. ) ;
#2436=EDGE_CURVE ( 'NONE', #2740, #5005, #604, .T. ) ;
#2438=DIRECTION ( 'NONE',  ( 0.000000000000000000, 0.000000000000000000, 1.000000000000000000 ) ) ;
#2440=LINE ( 'NONE', #6225, #7415 ) ;
#2447=DIRECTION ( 'NONE',  ( -0.000000000000000000, -0.000000000000000000, 1.000000000000000000 ) ) ;
#2453=AXIS2_PLACEMENT_3D ( 'NONE', #9470, #1017, #5831 ) ;
#2466=ORIENTED_EDGE ( 'NONE', *, *, #2980, .T. ) ;
#2475=AXIS2_PLACEMENT_3D ( 'NONE', #185, #10586, #1435 ) ;
#2484=( NAMED_UNIT ( * ) PLANE_ANGLE_UNIT ( ) SI_UNIT ( $, .RADIAN. ) );
#2498=DIRECTION ( 'NONE',  ( -0.8191520442889974607, 0.000000000000000000, -0.5735764363510379438 ) ) ;
#2510=EDGE_CURVE ( 'NONE', #4836, #2315, #8236, .T. ) ;
#2513=AXIS2_PLACEMENT_3D ( 'NONE', #10407, #8446, #1063 ) ;
#2520=DIRECTION ( 'NONE',  ( 0.000000000000000000, 0.000000000000000000, 1.000000000000000000 ) ) ;
#2536=EDGE_LOOP ( 'NONE', ( #8622, #1783, #1574, #5536 ) ) ;
#2539=DIRECTION ( 'NONE',  ( -1.000000000000000000, 0.000000000000000000, 0.000000000000000000 ) ) ;
#2542=SURFACE_STYLE_FILL_AREA ( #9722 ) ;
#2544=ORIENTED_EDGE ( 'NONE', *, *, #4268, .T. ) ;
#2555=EDGE_CURVE ( 'NONE', #3874, #7344, #10782, .T. ) ;
#2558=DIRECTION ( 'NONE',  ( 0.8191520442889974607, 1.003171929053531649E-16, -0.5735764363510379438 ) ) ;
#2571=EDGE_CURVE ( 'NONE', #6608, #1419, #8825, .T. ) ;
#2572=EDGE_CURVE ( 'NONE', #7093, #8959, #7760, .T. ) ;
#2581=ADVANCED_FACE ( 'NONE', ( #1123 ), #5007, .F. ) ;
#2591=CARTESIAN_POINT ( 'NONE',  ( 2.500000000000000000, 0.000000000000000000, -2.267810516609437776 ) ) ;
#2598=DIRECTION ( 'NONE',  ( -0.000000000000000000, -0.000000000000000000, -1.000000000000000000 ) ) ;
#2601=CARTESIAN_POINT ( 'NONE',  ( -5.000000000000000000, -2.886751345948134428, -5.653418012614792154 ) ) ;
#2612=LINE ( 'NONE', #11465, #1821 ) ;
#2613=EDGE_CURVE ( 'NONE', #3954, #2110, #5571, .T. ) ;
#2619=VECTOR ( 'NONE', #11191, 1000.000000000000000 ) ;
#2624=DIRECTION ( 'NONE',  ( -0.000000000000000000, 0.000000000000000000, -1.000000000000000000 ) ) ;
#2627=DIRECTION ( 'NONE',  ( -0.000000000000000000, -0.000000000000000000, 1.000000000000000000 ) ) ;
#2628=DIRECTION ( 'NONE',  ( 0.000000000000000000, 0.000000000000000000, 1.000000000000000000 ) ) ;
#2631=ORIENTED_EDGE ( 'NONE', *, *, #9786, .T. ) ;
#2640=AXIS2_PLACEMENT_3D ( 'NONE', #11010, #113, #1136 ) ;
#2646=EDGE_CURVE ( 'NONE', #1761, #5798, #4042, .T. ) ;
#2655=EDGE_CURVE ( 'NONE', #11822, #9962, #4854, .T. ) ;
#2656=CARTESIAN_POINT ( 'NONE',  ( -5.000000000000000000, 2.886751345948126879, -0.4465819873852047150 ) ) ;
#2665=B_SPLINE_CURVE_WITH_KNOTS ( 'NONE', 3,
 ( #6657, #7554, #407, #4974 ),
 .UNSPECIFIED., .F., .F.,
 ( 4, 4 ),
 ( 2.380735201027449880E-07, 0.002921158011986725936 ),
 .UNSPECIFIED. ) ;
#2675=EDGE_CURVE ( 'NONE', #11519, #9206, #2116, .T. ) ;
#2677=CARTESIAN_POINT ( 'NONE',  ( 0.000000000000000000, 0.000000000000000000, 0.000000000000000000 ) ) ;
#2691=ORIENTED_EDGE ( 'NONE', *, *, #3208, .F. ) ;
#2713=CARTESIAN_POINT ( 'NONE',  ( 1.653121499799245830, -4.819072548984015825, -6.048595712916167599 ) ) ;
#2722=CONICAL_SURFACE ( 'NONE', #6149, 5.000000000000000888, 1.047197551196596299 ) ;
#2730=EDGE_LOOP ( 'NONE', ( #6514, #10020, #9547, #4423 ) ) ;
#2740=VERTEX_POINT ( 'NONE', #1241 ) ;
#2745=DIRECTION ( 'NONE',  ( 1.000000000000000000, 0.000000000000000000, 0.000000000000000000 ) ) ;
#2746=CARTESIAN_POINT ( 'NONE',  ( -3.000000000000000000, 0.000000000000000000, -2.617914285714285416 ) ) ;
#2747=ORIENTED_EDGE ( 'NONE', *, *, #3301, .F. ) ;
#2752=DIRECTION ( 'NONE',  ( -1.000000000000000000, 0.000000000000000000, 0.000000000000000000 ) ) ;
#2755=DIRECTION ( 'NONE',  ( -1.000000000000000000, 0.000000000000000000, 0.000000000000000000 ) ) ;
#2765=EDGE_CURVE ( 'NONE', #1955, #364, #5771, .T. ) ;
#2771=ADVANCED_FACE ( 'NONE', ( #4729 ), #10343, .F. ) ;
#2778=ORIENTED_EDGE ( 'NONE', *, *, #10548, .T. ) ;
#2780=ORIENTED_EDGE ( 'NONE', *, *, #7328, .T. ) ;
#2787=ORIENTED_EDGE ( 'NONE', *, *, #236, .F. ) ;
#2791=AXIS2_PLACEMENT_3D ( 'NONE', #5976, #8955, #4402 ) ;
#2796=DIRECTION ( 'NONE',  ( -0.000000000000000000, -0.000000000000000000, -1.000000000000000000 ) ) ;
#2798=CARTESIAN_POINT ( 'NONE',  ( 0.000000000000000000, 0.000000000000000000, -2.968018054819144158 ) ) ;
#2802=DIRECTION ( 'NONE',  ( -0.000000000000000000, -0.000000000000000000, -1.000000000000000000 ) ) ;
#2814=AXIS2_PLACEMENT_3D ( 'NONE', #7954, #972, #3730 ) ;
#2816=ORIENTED_EDGE ( 'NONE', *, *, #6362, .T. ) ;
#2821=CYLINDRICAL_SURFACE ( 'NONE', #3959, 2.500000000000000000 ) ;
#2833=EDGE_LOOP ( 'NONE', ( #2544, #11590, #7513, #1642 ) ) ;
#2844=CIRCLE ( 'NONE', #10491, 5.000000000000000888 ) ;
#2851=AXIS2_PLACEMENT_3D ( 'NONE', #3849, #10959, #1081 ) ;
#2863=CARTESIAN_POINT ( 'NONE',  ( 2.500000000000000000, 0.000000000000000000, -6.099999999999999645 ) ) ;
#2872=CARTESIAN_POINT ( 'NONE',  ( 5.000000000000000888, 0.000000000000000000, -6.099999999999999645 ) ) ;
#2890=LINE ( 'NONE', #11013, #359 ) ;
#2897=AXIS2_PLACEMENT_3D ( 'NONE', #6862, #10374, #9541 ) ;
#2898=CARTESIAN_POINT ( 'NONE',  ( -5.000000000000000000, 1.947085426416881093, -5.900379292880307602 ) ) ;
#2928=DIRECTION ( 'NONE',  ( 0.000000000000000000, 0.000000000000000000, -1.000000000000000000 ) ) ;
#2930=ORIENTED_EDGE ( 'NONE', *, *, #2555, .T. ) ;
#2934=CARTESIAN_POINT ( 'NONE',  ( -2.500000000000003553, 4.330127018922192761, 0.000000000000000000 ) ) ;
#2947=EDGE_CURVE ( 'NONE', #5798, #1761, #8151, .T. ) ;
#2948=DIRECTION ( 'NONE',  ( 0.000000000000000000, 0.000000000000000000, 1.000000000000000000 ) ) ;
#2950=EDGE_CURVE ( 'NONE', #1664, #6890, #3941, .T. ) ;
#2966=LINE ( 'NONE', #10438, #1641 ) ;
#2980=EDGE_CURVE ( 'NONE', #7344, #9472, #3338, .T. ) ;
#2988=ORIENTED_EDGE ( 'NONE', *, *, #3901, .T. ) ;
#2996=ORIENTED_EDGE ( 'NONE', *, *, #4979, .T. ) ;
#3002=DIRECTION ( 'NONE',  ( 0.000000000000000000, 0.000000000000000000, 1.000000000000000000 ) ) ;
#3004=DIRECTION ( 'NONE',  ( 0.000000000000000000, 0.000000000000000000, 1.000000000000000000 ) ) ;
#3020=ORIENTED_EDGE ( 'NONE', *, *, #1903, .F. ) ;
#3037=CARTESIAN_POINT ( 'NONE',  ( -2.500000000000000000, 3.061616997868383141E-16, -2.103846626247716234 ) ) ;
#3052=DIRECTION ( 'NONE',  ( -0.8191520442889974607, 0.000000000000000000, -0.5735764363510379438 ) ) ;
#3060=AXIS2_PLACEMENT_3D ( 'NONE', #10748, #6223, #7180 ) ;
#3065=DIRECTION ( 'NONE',  ( -0.000000000000000000, -0.000000000000000000, -1.000000000000000000 ) ) ;
#3067=EDGE_LOOP ( 'NONE', ( #10211, #5606, #167, #7804 ) ) ;
#3085=CYLINDRICAL_SURFACE ( 'NONE', #2320, 2.500000000000000000 ) ;
#3088=AXIS2_PLACEMENT_3D ( 'NONE', #8704, #7928, #9655 ) ;
#3113=DIRECTION ( 'NONE',  ( 1.000000000000000000, 0.000000000000000000, 0.000000000000000000 ) ) ;
#3118=EDGE_LOOP ( 'NONE', ( #11704, #1583, #3135, #3342 ) ) ;
#3131=EDGE_CURVE ( 'NONE', #9206, #6608, #7661, .T. ) ;
#3135=ORIENTED_EDGE ( 'NONE', *, *, #1110, .T. ) ;
#3138=ORIENTED_EDGE ( 'NONE', *, *, #7338, .T. ) ;
#3142=DIRECTION ( 'NONE',  ( -0.000000000000000000, 0.000000000000000000, -1.000000000000000000 ) ) ;
#3144=DIRECTION ( 'NONE',  ( -0.000000000000000000, -0.000000000000000000, -1.000000000000000000 ) ) ;
#3155=DIRECTION ( 'NONE',  ( 1.000000000000000000, 0.000000000000000000, 0.000000000000000000 ) ) ;
#3160=PRODUCT_DEFINITION_FORMATION_WITH_SPECIFIED_SOURCE ( 'ANY', '', #10530, .NOT_KNOWN. ) ;
#3166=EDGE_CURVE ( 'NONE', #8985, #6801, #11294, .T. ) ;
#3168=CARTESIAN_POINT ( 'NONE',  ( 0.000000000000000000, 0.000000000000000000, -0.01270000000000047133 ) ) ;
#3182=CARTESIAN_POINT ( 'NONE',  ( 2.500000000000003109, -4.330127018922193649, -6.099999999999999645 ) ) ;
#3185=CARTESIAN_POINT ( 'NONE',  ( 0.000000000000000000, 0.000000000000000000, -0.8895714285714284575 ) ) ;
#3186=ORIENTED_EDGE ( 'NONE', *, *, #2555, .F. ) ;
#3191=ORIENTED_EDGE ( 'NONE', *, *, #445, .F. ) ;
#3195=CONICAL_SURFACE ( 'NONE', #9883, 3.000000000000000000, 0.9599310885968912466 ) ;
#3198=CARTESIAN_POINT ( 'NONE',  ( 2.500000000000000000, 0.000000000000000000, -1.403639088038009630 ) ) ;
#3200=DIRECTION ( 'NONE',  ( -0.000000000000000000, -0.000000000000000000, 1.000000000000000000 ) ) ;
#3205=B_SPLINE_CURVE_WITH_KNOTS ( 'NONE', 3,
 ( #3978, #7635, #2052, #7464, #3859, #7522 ),
 .UNSPECIFIED., .F., .F.,
 ( 4, 2, 4 ),
 ( 0.005150343764683554260, 0.006610526168996383976, 0.008070708573309213693 ),
 .UNSPECIFIED. ) ;
#3208=EDGE_CURVE ( 'NONE', #10937, #6451, #2612, .T. ) ;
#3217=DIRECTION ( 'NONE',  ( 1.000000000000000000, 0.000000000000000000, 0.000000000000000000 ) ) ;
#3234=CARTESIAN_POINT ( 'NONE',  ( 0.000000000000000000, 0.000000000000000000, -4.346257142857142597 ) ) ;
#3237=DIRECTION ( 'NONE',  ( 0.8191520442889974607, 1.003171929053531649E-16, -0.5735764363510379438 ) ) ;
#3239=DIRECTION ( 'NONE',  ( -0.000000000000000000, -0.000000000000000000, -1.000000000000000000 ) ) ;
#3242=CARTESIAN_POINT ( 'NONE',  ( 4.182066831946701591, -3.358985280702831755, -0.1739375980333770777 ) ) ;
#3246=ORIENTED_EDGE ( 'NONE', *, *, #8926, .F. ) ;
#3253=CARTESIAN_POINT ( 'NONE',  ( 0.000000000000000000, 5.773502691896260863, -5.653418012614792154 ) ) ;
#3254=ORIENTED_EDGE ( 'NONE', *, *, #2212, .T. ) ;
#3256=CARTESIAN_POINT ( 'NONE',  ( 2.500000000000000000, 0.000000000000000000, -2.968018054819144158 ) ) ;
#3271=ORIENTED_EDGE ( 'NONE', *, *, #9932, .T. ) ;
#3275=( NAMED_UNIT ( * ) SI_UNIT ( $, .STERADIAN. ) SOLID_ANGLE_UNIT ( ) );
#3276=CIRCLE ( 'NONE', #9782, 5.000000000000000888 ) ;
#3284=CARTESIAN_POINT ( 'NONE',  ( 1.653121499799245164, -4.819072548984015825, -0.05140428708383163597 ) ) ;
#3298=PRODUCT_DEFINITION ( 'UNKNOWN', '', #3160, #7033 ) ;
#3301=EDGE_CURVE ( 'NONE', #11519, #1419, #628, .T. ) ;
#3312=CARTESIAN_POINT ( 'NONE',  ( -3.000000000000000000, 0.000000000000000000, -0.02539999999999996774 ) ) ;
#3338=LINE ( 'NONE', #9690, #5868 ) ;
#3342=ORIENTED_EDGE ( 'NONE', *, *, #589, .F. ) ;
#3358=CARTESIAN_POINT ( 'NONE',  ( 0.000000000000000000, 0.000000000000000000, -2.103846626247716234 ) ) ;
#3366=DIRECTION ( 'NONE',  ( 1.000000000000000000, 0.000000000000000000, 0.000000000000000000 ) ) ;
#3385=AXIS2_PLACEMENT_3D ( 'NONE', #9432, #10208, #10143 ) ;
#3386=ORIENTED_EDGE ( 'NONE', *, *, #8584, .T. ) ;
#3390=ORIENTED_EDGE ( 'NONE', *, *, #3458, .T. ) ;
#3391=( LENGTH_UNIT ( ) NAMED_UNIT ( * ) SI_UNIT ( .MILLI., .METRE. ) );
#3399=FACE_OUTER_BOUND ( 'NONE', #836, .T. ) ;
#3412=LINE ( 'NONE', #10769, #7255 ) ;
#3423=PLANE ( 'NONE',  #7875 ) ;
#3424=CARTESIAN_POINT ( 'NONE',  ( 2.287832656137189336, -4.452621892014644978, -6.099999999999998757 ) ) ;
#3426=AXIS2_PLACEMENT_3D ( 'NONE', #7010, #6290, #9693 ) ;
#3427=CARTESIAN_POINT ( 'NONE',  ( 5.000000000000000000, 2.886751345948134428, -5.653418012614792154 ) ) ;
#3429=ORIENTED_EDGE ( 'NONE', *, *, #1684, .F. ) ;
#3431=ADVANCED_FACE ( 'NONE', ( #11571 ), #7966, .T. ) ;
#3432=CARTESIAN_POINT ( 'NONE',  ( 3.000000000000000000, 3.673940397442059868E-16, -2.617914285714285416 ) ) ;
#3450=EDGE_CURVE ( 'NONE', #9962, #7344, #5289, .T. ) ;
#3458=EDGE_CURVE ( 'NONE', #6384, #3954, #2966, .T. ) ;
#3462=EDGE_LOOP ( 'NONE', ( #2129, #11848, #5106, #1990 ) ) ;
#3467=CARTESIAN_POINT ( 'NONE',  ( 0.4079457818577022499, -5.537975084925951919, -0.3106000600989376470 ) ) ;
#3468=CARTESIAN_POINT ( 'NONE',  ( 3.000000000000000000, 0.000000000000000000, 0.000000000000000000 ) ) ;
#3470=AXIS2_PLACEMENT_3D ( 'NONE', #162, #1965, #1189 ) ;
#3478=CIRCLE ( 'NONE', #6160, 2.500000000000000000 ) ;
#3479=DIRECTION ( 'NONE',  ( 0.000000000000000000, 0.000000000000000000, 1.000000000000000000 ) ) ;
#3480=ORIENTED_EDGE ( 'NONE', *, *, #4994, .T. ) ;
#3484=DIRECTION ( 'NONE',  ( 0.000000000000000000, 0.000000000000000000, -1.000000000000000000 ) ) ;
#3496=CARTESIAN_POINT ( 'NONE',  ( 0.000000000000000000, 0.000000000000000000, 0.000000000000000000 ) ) ;
#3502=PLANE ( 'NONE',  #8367 ) ;
#3503=CARTESIAN_POINT ( 'NONE',  ( -2.500000000000000000, 3.061616997868383141E-16, -1.239675197676287643 ) ) ;
#3504=ORIENTED_EDGE ( 'NONE', *, *, #1032, .T. ) ;
#3519=DIRECTION ( 'NONE',  ( -0.000000000000000000, -0.000000000000000000, -1.000000000000000000 ) ) ;
#3521=ORIENTED_EDGE ( 'NONE', *, *, #8531, .T. ) ;
#3522=DIRECTION ( 'NONE',  ( 0.000000000000000000, 0.000000000000000000, 1.000000000000000000 ) ) ;
#3524=LINE ( 'NONE', #5155, #11694 ) ;
#3527=DIRECTION ( 'NONE',  ( -0.000000000000000000, -0.000000000000000000, 1.000000000000000000 ) ) ;
#3530=ADVANCED_FACE ( 'NONE', ( #2180 ), #9554, .F. ) ;
#3531=EDGE_LOOP ( 'NONE', ( #106, #7867 ) ) ;
#3532=DIRECTION ( 'NONE',  ( -0.000000000000000000, -0.000000000000000000, -1.000000000000000000 ) ) ;
#3546=DIRECTION ( 'NONE',  ( 1.000000000000000000, 0.000000000000000000, 0.000000000000000000 ) ) ;
#3554=DIRECTION ( 'NONE',  ( 1.000000000000000000, 0.000000000000000000, 0.000000000000000000 ) ) ;
#3564=AXIS2_PLACEMENT_3D ( 'NONE', #11336, #3144, #11573 ) ;
#3567=EDGE_CURVE ( 'NONE', #7792, #2110, #8715, .T. ) ;
#3572=EDGE_CURVE ( 'NONE', #6455, #7832, #9293, .T. ) ;
#3574=ORIENTED_EDGE ( 'NONE', *, *, #2980, .F. ) ;
#3579=FACE_OUTER_BOUND ( 'NONE', #3462, .T. ) ;
#3583=CARTESIAN_POINT ( 'NONE',  ( 0.000000000000000000, 0.000000000000000000, -4.860324802323723326 ) ) ;
#3594=DIRECTION ( 'NONE',  ( -0.000000000000000000, -0.000000000000000000, -1.000000000000000000 ) ) ;
#3599=ORIENTED_EDGE ( 'NONE', *, *, #8805, .T. ) ;
#3601=ORIENTED_EDGE ( 'NONE', *, *, #8627, .T. ) ;
#3619=CARTESIAN_POINT ( 'NONE',  ( 4.592054218142289201, 3.122278952918447370, -0.3106000600989279326 ) ) ;
#3623=AXIS2_PLACEMENT_3D ( 'NONE', #4775, #4595, #2745 ) ;
#3629=DIRECTION ( 'NONE',  ( 0.000000000000000000, 0.000000000000000000, 1.000000000000000000 ) ) ;
#3639=ORIENTED_EDGE ( 'NONE', *, *, #1838, .T. ) ;
#3640=ADVANCED_FACE ( 'NONE', ( #11277 ), #4917, .T. ) ;
#3659=CIRCLE ( 'NONE', #3847, 3.000000000000000000 ) ;
#3666=DIRECTION ( 'NONE',  ( -0.8191520442889885789, 1.003171929053520802E-16, 0.5735764363510507113 ) ) ;
#3672=ADVANCED_FACE ( 'NONE', ( #10385 ), #8731, .T. ) ;
#3680=EDGE_CURVE ( 'NONE', #10987, #5713, #1268, .T. ) ;
#3681=VERTEX_POINT ( 'NONE', #4463 ) ;
#3694=CARTESIAN_POINT ( 'NONE',  ( 5.000000000000000888, 0.000000000000000000, 0.000000000000000000 ) ) ;
#3696=CARTESIAN_POINT ( 'NONE',  ( 3.000000000000000000, 3.673940397442059868E-16, -0.8895714285714284575 ) ) ;
#3697=CARTESIAN_POINT ( 'NONE',  ( 2.500000000000000000, 0.000000000000000000, -2.968018054819144158 ) ) ;
#3702=DIRECTION ( 'NONE',  ( 0.000000000000000000, 0.000000000000000000, 1.000000000000000000 ) ) ;
#3705=FACE_OUTER_BOUND ( 'NONE', #2536, .T. ) ;
#3706=CIRCLE ( 'NONE', #4482, 2.500000000000000000 ) ;
#3711=ORIENTED_EDGE ( 'NONE', *, *, #6362, .F. ) ;
#3719=ADVANCED_FACE ( 'NONE', ( #5184 ), #6932, .F. ) ;
#3724=DIRECTION ( 'NONE',  ( 0.000000000000000000, 0.000000000000000000, 1.000000000000000000 ) ) ;
#3728=CARTESIAN_POINT ( 'NONE',  ( -2.500000000000000000, 3.061616997868383141E-16, -6.099999999999999645 ) ) ;
#3730=DIRECTION ( 'NONE',  ( -1.000000000000000000, 0.000000000000000000, 0.000000000000000000 ) ) ;
#3733=VERTEX_POINT ( 'NONE', #2601 ) ;
#3750=CARTESIAN_POINT ( 'NONE',  ( 5.000000000000000000, -2.417244626924489381, -5.788952927922133895 ) ) ;
#3765=DIRECTION ( 'NONE',  ( 1.000000000000000000, 0.000000000000000000, 0.000000000000000000 ) ) ;
#3766=DIRECTION ( 'NONE',  ( 0.000000000000000000, 0.000000000000000000, 1.000000000000000000 ) ) ;
#3767=DIRECTION ( 'NONE',  ( -0.8191520442889885789, 1.003171929053520802E-16, 0.5735764363510507113 ) ) ;
#3768=DIRECTION ( 'NONE',  ( -1.000000000000000000, 0.000000000000000000, 0.000000000000000000 ) ) ;
#3774=ORIENTED_EDGE ( 'NONE', *, *, #6456, .T. ) ;
#3791=CARTESIAN_POINT ( 'NONE',  ( -4.999999999999999112, 0.4881033300985035961, -6.099999999999999645 ) ) ;
#3801=STYLED_ITEM('',(#11895),#4897);
#3802=CARTESIAN_POINT ( 'NONE',  ( 0.000000000000000000, 0.000000000000000000, -0.3755037691048591086 ) ) ;
#3810=ADVANCED_FACE ( 'NONE', ( #9011 ), #6069, .F. ) ;
#3815=DIRECTION ( 'NONE',  ( -1.000000000000000000, 0.000000000000000000, 0.000000000000000000 ) ) ;
#3828=DIRECTION ( 'NONE',  ( -0.000000000000000000, -0.000000000000000000, -1.000000000000000000 ) ) ;
#3835=DIRECTION ( 'NONE',  ( -1.000000000000000000, 0.000000000000000000, 0.000000000000000000 ) ) ;
#3845=DIRECTION ( 'NONE',  ( 1.000000000000000000, 0.000000000000000000, 0.000000000000000000 ) ) ;
#3847=AXIS2_PLACEMENT_3D ( 'NONE', #3185, #10483, #2285 ) ;
#3849=CARTESIAN_POINT ( 'NONE',  ( 0.000000000000000000, 0.000000000000000000, -3.996153373752295401 ) ) ;
#3852=FACE_OUTER_BOUND ( 'NONE', #11050, .T. ) ;
#3859=CARTESIAN_POINT ( 'NONE',  ( -5.000000000000000000, -0.4878135028931869788, -6.100000000000001421 ) ) ;
#3860=CARTESIAN_POINT ( 'NONE',  ( -2.500000000000003553, 4.330127018922192761, -6.099999999999999645 ) ) ;
#3871=EDGE_LOOP ( 'NONE', ( #1167, #1972, #3504, #375 ) ) ;
#3874=VERTEX_POINT ( 'NONE', #9356 ) ;
#3884=DIRECTION ( 'NONE',  ( 0.8660254037844382635, 0.5000000000000004441, 0.000000000000000000 ) ) ;
#3893=CARTESIAN_POINT ( 'NONE',  ( 3.000000000000000000, 3.673940397442059868E-16, -0.8895714285714284575 ) ) ;
#3901=EDGE_CURVE ( 'NONE', #3923, #1322, #8069, .T. ) ;
#3902=DIRECTION ( 'NONE',  ( -0.000000000000000000, -0.000000000000000000, 1.000000000000000000 ) ) ;
#3905=ORIENTED_EDGE ( 'NONE', *, *, #2436, .F. ) ;
#3911=DIRECTION ( 'NONE',  ( -1.000000000000000000, 0.000000000000000000, 0.000000000000000000 ) ) ;
#3923=VERTEX_POINT ( 'NONE', #4088 ) ;
#3924=DIRECTION ( 'NONE',  ( 1.000000000000000000, 0.000000000000000000, 0.000000000000000000 ) ) ;
#3941=CIRCLE ( 'NONE', #10620, 2.500000000000000000 ) ;
#3944=ORIENTED_EDGE ( 'NONE', *, *, #1308, .F. ) ;
#3948=ADVANCED_FACE ( 'NONE', ( #6743 ), #201, .F. ) ;
#3953=AXIS2_PLACEMENT_3D ( 'NONE', #1522, #7052, #8839 ) ;
#3954=VERTEX_POINT ( 'NONE', #4936 ) ;
#3959=AXIS2_PLACEMENT_3D ( 'NONE', #1976, #7510, #9229 ) ;
#3962=FACE_OUTER_BOUND ( 'NONE', #3871, .T. ) ;
#3964=ADVANCED_FACE ( 'NONE', ( #4034 ), #11103, .T. ) ;
#3969=CONICAL_SURFACE ( 'NONE', #1083, 5.000000000000000888, 1.047197551196596299 ) ;
#3974=AXIS2_PLACEMENT_3D ( 'NONE', #11143, #9243, #2172 ) ;
#3977=ORIENTED_EDGE ( 'NONE', *, *, #3301, .T. ) ;
#3978=CARTESIAN_POINT ( 'NONE',  ( -5.000000000000000000, -2.886751345948134428, -5.653418012614792154 ) ) ;
#3998=CIRCLE ( 'NONE', #3060, 2.500000000000000000 ) ;
#4003=CIRCLE ( 'NONE', #2851, 2.500000000000000000 ) ;
#4006=CIRCLE ( 'NONE', #4774, 2.500000000000000000 ) ;
#4010=CARTESIAN_POINT ( 'NONE',  ( -2.500000000000000000, 3.061616997868383141E-16, -4.696360911962001339 ) ) ;
#4013=CARTESIAN_POINT ( 'NONE',  ( 2.500000000000000000, 0.000000000000000000, -6.099999999999999645 ) ) ;
#4017=EDGE_LOOP ( 'NONE', ( #6701, #509, #9041, #4807 ) ) ;
#4022=CARTESIAN_POINT ( 'NONE',  ( 4.999999999999998224, -2.886751345948137981, -5.653418012614792154 ) ) ;
#4034=FACE_OUTER_BOUND ( 'NONE', #189, .T. ) ;
#4035=DIRECTION ( 'NONE',  ( -0.8191520442889974607, 0.000000000000000000, -0.5735764363510379438 ) ) ;
#4042=CIRCLE ( 'NONE', #1925, 3.000000000000000000 ) ;
#4050=ORIENTED_EDGE ( 'NONE', *, *, #4153, .F. ) ;
#4051=EDGE_CURVE ( 'NONE', #6251, #52, #8441, .T. ) ;
#4052=CARTESIAN_POINT ( 'NONE',  ( 0.000000000000000000, 0.000000000000000000, -6.099999999999999645 ) ) ;
#4054=CARTESIAN_POINT ( 'NONE',  ( -1.443735181952766178, 4.939961795957295010, -0.08165819712376964912 ) ) ;
#4060=AXIS2_PLACEMENT_3D ( 'NONE', #11748, #4512, #3554 ) ;
#4063=CARTESIAN_POINT ( 'NONE',  ( -1.734723475976807094E-14, -5.773502691896260863, -0.4465819873852071575 ) ) ;
#4069=ORIENTED_EDGE ( 'NONE', *, *, #1402, .F. ) ;
#4088=CARTESIAN_POINT ( 'NONE',  ( 2.500000000000003109, -4.330127018922193649, 0.000000000000000000 ) ) ;
#4091=ORIENTED_EDGE ( 'NONE', *, *, #298, .T. ) ;
#4093=CARTESIAN_POINT ( 'NONE',  ( -1.443735181952766622, 4.939961795957295898, -6.018341802876231661 ) ) ;
#4103=EDGE_CURVE ( 'NONE', #9830, #1810, #5115, .T. ) ;
#4126=ORIENTED_EDGE ( 'NONE', *, *, #8627, .F. ) ;
#4132=DIRECTION ( 'NONE',  ( -0.000000000000000000, -0.000000000000000000, -1.000000000000000000 ) ) ;
#4139=CARTESIAN_POINT ( 'NONE',  ( 3.351853367131007122, -3.838309248099025961, -4.312635593573742646E-16 ) ) ;
#4145=CARTESIAN_POINT ( 'NONE',  ( -3.351853367131005346, 3.838309248099017523, -6.100000000000003197 ) ) ;
#4149=CARTESIAN_POINT ( 'NONE',  ( -1.653121499799247163, 4.819072548984006943, -6.048595712916175593 ) ) ;
#4153=EDGE_CURVE ( 'NONE', #7832, #6455, #1160, .T. ) ;
#4155=FACE_OUTER_BOUND ( 'NONE', #4323, .T. ) ;
#4159=DIRECTION ( 'NONE',  ( -0.000000000000000000, -0.000000000000000000, -1.000000000000000000 ) ) ;
#4164=VERTEX_POINT ( 'NONE', #1569 ) ;
#4167=CARTESIAN_POINT ( 'NONE',  ( 2.500000000000000000, 0.000000000000000000, -3.832189483390572970 ) ) ;
#4168=CARTESIAN_POINT ( 'NONE',  ( 2.500000000000005773, 4.330127018922190985, 0.000000000000000000 ) ) ;
#4169=VECTOR ( 'NONE', #3237, 1000.000000000000114 ) ;
#4175=CYLINDRICAL_SURFACE ( 'NONE', #9352, 2.500000000000000000 ) ;
#4177=ADVANCED_FACE ( 'NONE', ( #8882, #11620 ), #3423, .T. ) ;
#4183=DIRECTION ( 'NONE',  ( 0.000000000000000000, 0.000000000000000000, 1.000000000000000000 ) ) ;
#4189=ORIENTED_EDGE ( 'NONE', *, *, #8952, .F. ) ;
#4196=VECTOR ( 'NONE', #3629, 1000.000000000000000 ) ;
#4197=B_SPLINE_CURVE_WITH_KNOTS ( 'NONE', 3,
 ( #11753, #9125, #8061, #11814, #11636, #10014, #3619, #11703 ),
 .UNSPECIFIED., .F., .F.,
 ( 4, 2, 2, 4 ),
 ( 0.002921158011986720298, 0.003648658599403072685, 0.004376159186819424639, 0.005831160361652126811 ),
 .UNSPECIFIED. ) ;
#4209=CARTESIAN_POINT ( 'NONE',  ( -2.500000000000003553, 4.330127018922192761, -6.099999999999999645 ) ) ;
#4211=EDGE_LOOP ( 'NONE', ( #8120, #11383, #3138, #10584 ) ) ;
#4216=CYLINDRICAL_SURFACE ( 'NONE', #11471, 2.500000000000000000 ) ;
#4224=CARTESIAN_POINT ( 'NONE',  ( -2.712167343862823543, -4.207632145829752979, -9.186072312972883233E-16 ) ) ;
#4238=VECTOR ( 'NONE', #5688, 1000.000000000000114 ) ;
#4242=EDGE_LOOP ( 'NONE', ( #9934, #11565, #7251, #8253 ) ) ;
#4258=EDGE_CURVE ( 'NONE', #8985, #10937, #3478, .T. ) ;
#4268=EDGE_CURVE ( 'NONE', #5840, #1730, #5775, .T. ) ;
#4272=DIRECTION ( 'NONE',  ( 1.000000000000000000, 0.000000000000000000, 0.000000000000000000 ) ) ;
#4275=ORIENTED_EDGE ( 'NONE', *, *, #8549, .T. ) ;
#4280=PRESENTATION_STYLE_ASSIGNMENT (( #9783 ) ) ;
#4283=CARTESIAN_POINT ( 'NONE',  ( -2.500000000000005773, -4.330127018922191873, 0.000000000000000000 ) ) ;
#4293=EDGE_LOOP ( 'NONE', ( #7841, #9185, #2241, #2181 ) ) ;
#4294=DIRECTION ( 'NONE',  ( 0.000000000000000000, -0.000000000000000000, 1.000000000000000000 ) ) ;
#4299=EDGE_CURVE ( 'NONE', #7344, #9962, #6737, .T. ) ;
#4322=CARTESIAN_POINT ( 'NONE',  ( 5.000000000000000000, -2.886751345948136205, -6.099999999999999645 ) ) ;
#4323=EDGE_LOOP ( 'NONE', ( #5427, #10538, #4909 ) ) ;
#4339=CARTESIAN_POINT ( 'NONE',  ( -5.000000000000000000, 2.419979747126323577, -0.3118366332702841026 ) ) ;
#4346=ADVANCED_FACE ( 'NONE', ( #10363 ), #7621, .F. ) ;
#4355=AXIS2_PLACEMENT_3D ( 'NONE', #1185, #3828, #1058 ) ;
#4367=DIRECTION ( 'NONE',  ( -0.000000000000000000, -0.000000000000000000, 1.000000000000000000 ) ) ;
#4370=ORIENTED_EDGE ( 'NONE', *, *, #1191, .F. ) ;
#4378=CARTESIAN_POINT ( 'NONE',  ( -3.000000000000000000, 0.000000000000000000, -0.02539999999999996774 ) ) ;
#4393=CONICAL_SURFACE ( 'NONE', #3623, 2.500000000000000000, 0.9599310885968755924 ) ;
#4402=DIRECTION ( 'NONE',  ( 1.000000000000000000, 0.000000000000000000, 0.000000000000000000 ) ) ;
#4418=ADVANCED_FACE ( 'NONE', ( #10707 ), #5012, .F. ) ;
#4420=CARTESIAN_POINT ( 'NONE',  ( -2.500000000000000000, 3.061616997868383141E-16, -6.099999999999999645 ) ) ;
#4423=ORIENTED_EDGE ( 'NONE', *, *, #7927, .F. ) ;
#4428=DIRECTION ( 'NONE',  ( -1.000000000000000000, 0.000000000000000000, 0.000000000000000000 ) ) ;
#4437=AXIS2_PLACEMENT_3D ( 'NONE', #2351, #11558, #7155 ) ;
#4438=FACE_OUTER_BOUND ( 'NONE', #9300, .T. ) ;
#4441=EDGE_CURVE ( 'NONE', #4164, #11218, #6547, .T. ) ;
#4447=ORIENTED_EDGE ( 'NONE', *, *, #3131, .T. ) ;
#4453=DIRECTION ( 'NONE',  ( -0.8191520442889885789, 1.003171929053520802E-16, 0.5735764363510507113 ) ) ;
#4463=CARTESIAN_POINT ( 'NONE',  ( 2.500000000000005773, 4.330127018922190985, -6.099999999999999645 ) ) ;
#4468=ORIENTED_EDGE ( 'NONE', *, *, #2675, .F. ) ;
#4480=CARTESIAN_POINT ( 'NONE',  ( 5.000000000000000888, -1.936377641173860686, -5.902630826755077997 ) ) ;
#4482=AXIS2_PLACEMENT_3D ( 'NONE', #2380, #8800, #10632 ) ;
#4483=CARTESIAN_POINT ( 'NONE',  ( 0.000000000000000000, 0.000000000000000000, -2.267810516609437776 ) ) ;
#4484=EDGE_LOOP ( 'NONE', ( #5701, #4649, #3390, #7006 ) ) ;
#4488=ORIENTED_EDGE ( 'NONE', *, *, #946, .T. ) ;
#4490=EDGE_CURVE ( 'NONE', #7952, #5996, #211, .T. ) ;
#4494=LINE ( 'NONE', #1064, #9373 ) ;
#4497=DIRECTION ( 'NONE',  ( -0.000000000000000000, -0.000000000000000000, -1.000000000000000000 ) ) ;
#4512=DIRECTION ( 'NONE',  ( -0.000000000000000000, -0.000000000000000000, 1.000000000000000000 ) ) ;
#4520=ORIENTED_EDGE ( 'NONE', *, *, #75, .F. ) ;
#4521=ADVANCED_FACE ( 'NONE', ( #4438 ), #977, .F. ) ;
#4525=EDGE_CURVE ( 'NONE', #10937, #5713, #6299, .T. ) ;
#4526=ORIENTED_EDGE ( 'NONE', *, *, #11204, .F. ) ;
#4531=CARTESIAN_POINT ( 'NONE',  ( 3.000000000000000888, 0.000000000000000000, -25.03750572909317285 ) ) ;
#4548=CIRCLE ( 'NONE', #2814, 2.500000000000000000 ) ;
#4549=PLANE ( 'NONE',  #597 ) ;
#4553=ADVANCED_FACE ( 'NONE', ( #11667 ), #4549, .T. ) ;
#4555=EDGE_CURVE ( 'NONE', #7093, #3681, #3276, .T. ) ;
#4568=CARTESIAN_POINT ( 'NONE',  ( 0.8192951148925836646, -5.300482436767290473, -5.901655677627834606 ) ) ;
#4577=MECHANICAL_DESIGN_GEOMETRIC_PRESENTATION_REPRESENTATION('',(#3801),#8019);
#4588=FACE_OUTER_BOUND ( 'NONE', #10612, .T. ) ;
#4595=DIRECTION ( 'NONE',  ( 0.000000000000000000, 0.000000000000000000, 1.000000000000000000 ) ) ;
#4596=CARTESIAN_POINT ( 'NONE',  ( -2.500000000000005773, -4.330127018922191873, -6.099999999999999645 ) ) ;
#4601=CONICAL_SURFACE ( 'NONE', #955, 5.000000000000000888, 1.047197551196596299 ) ;
#4613=EDGE_LOOP ( 'NONE', ( #6741, #11745, #8633, #1148 ) ) ;
#4624=AXIS2_PLACEMENT_3D ( 'NONE', #7163, #2598, #9064 ) ;
#4630=FACE_OUTER_BOUND ( 'NONE', #11394, .T. ) ;
#4634=CARTESIAN_POINT ( 'NONE',  ( 0.000000000000000000, 0.000000000000000000, -4.346257142857142597 ) ) ;
#4638=CARTESIAN_POINT ( 'NONE',  ( -3.000000000000000000, 0.000000000000000000, -4.346257142857142597 ) ) ;
#4639=ORIENTED_EDGE ( 'NONE', *, *, #4051, .F. ) ;
#4649=ORIENTED_EDGE ( 'NONE', *, *, #10875, .T. ) ;
#4664=VECTOR ( 'NONE', #4183, 1000.000000000000000 ) ;
#4666=DIRECTION ( 'NONE',  ( 0.000000000000000000, -0.000000000000000000, 1.000000000000000000 ) ) ;
#4672=ORIENTED_EDGE ( 'NONE', *, *, #10007, .F. ) ;
#4679=DIRECTION ( 'NONE',  ( -1.000000000000000000, 0.000000000000000000, 0.000000000000000000 ) ) ;
#4680=ORIENTED_EDGE ( 'NONE', *, *, #4268, .F. ) ;
#4691=EDGE_CURVE ( 'NONE', #3874, #66, #6594, .T. ) ;
#4693=ORIENTED_EDGE ( 'NONE', *, *, #5576, .F. ) ;
#4703=CARTESIAN_POINT ( 'NONE',  ( 4.999999999999998224, -2.886751345948137981, -0.4465819873852071575 ) ) ;
#4718=EDGE_LOOP ( 'NONE', ( #3774, #5748, #985 ) ) ;
#4727=ORIENTED_EDGE ( 'NONE', *, *, #11418, .T. ) ;
#4729=FACE_OUTER_BOUND ( 'NONE', #4613, .T. ) ;
#4731=CARTESIAN_POINT ( 'NONE',  ( 0.000000000000000000, 0.000000000000000000, -5.210428571428570521 ) ) ;
#4738=AXIS2_PLACEMENT_3D ( 'NONE', #6164, #8011, #1383 ) ;
#4744=PLANE ( 'NONE',  #2453 ) ;
#4774=AXIS2_PLACEMENT_3D ( 'NONE', #9039, #5271, #10760 ) ;
#4775=CARTESIAN_POINT ( 'NONE',  ( 0.000000000000000000, 0.000000000000000000, -3.832189483390572970 ) ) ;
#4777=EDGE_CURVE ( 'NONE', #7952, #10233, #7428, .T. ) ;
#4782=B_SPLINE_CURVE_WITH_KNOTS ( 'NONE', 3,
 ( #834, #6260, #10003, #10723 ),
 .UNSPECIFIED., .F., .F.,
 ( 4, 4 ),
 ( 2.380735200850351173E-07, 0.002921158011986708155 ),
 .UNSPECIFIED. ) ;
#4783=CARTESIAN_POINT ( 'NONE',  ( -3.000000000000000000, 0.000000000000000000, -0.8895714285714284575 ) ) ;
#4785=FACE_OUTER_BOUND ( 'NONE', #2833, .T. ) ;
#4787=ORIENTED_EDGE ( 'NONE', *, *, #9382, .T. ) ;
#4792=FACE_OUTER_BOUND ( 'NONE', #1931, .T. ) ;
#4807=ORIENTED_EDGE ( 'NONE', *, *, #5783, .F. ) ;
#4809=VECTOR ( 'NONE', #11682, 1000.000000000000000 ) ;
#4836=VERTEX_POINT ( 'NONE', #5993 ) ;
#4847=CARTESIAN_POINT ( 'NONE',  ( -7.511572993685809947E-16, -5.773502691896268857, -6.099999999999999645 ) ) ;
#4850=ADVANCED_FACE ( 'NONE', ( #1365 ), #4175, .F. ) ;
#4854=LINE ( 'NONE', #7497, #11295 ) ;
#4855=DIRECTION ( 'NONE',  ( 1.000000000000000000, 0.000000000000000000, 0.000000000000000000 ) ) ;
#4865=CARTESIAN_POINT ( 'NONE',  ( 0.000000000000000000, 0.000000000000000000, -5.724496230895143256 ) ) ;
#4868=ORIENTED_EDGE ( 'NONE', *, *, #3567, .F. ) ;
#4873=ORIENTED_EDGE ( 'NONE', *, *, #8355, .F. ) ;
#4884=CARTESIAN_POINT ( 'NONE',  ( 5.000000000000000000, 1.947085426416880649, -0.1996207071196908767 ) ) ;
#4897=MANIFOLD_SOLID_BREP ( 'ThdSchPat', #5593 ) ;
#4904=EDGE_CURVE ( 'NONE', #8530, #7093, #2844, .T. ) ;
#4909=ORIENTED_EDGE ( 'NONE', *, *, #2765, .T. ) ;
#4912=DIRECTION ( 'NONE',  ( -1.000000000000000000, 0.000000000000000000, 0.000000000000000000 ) ) ;
#4913=FACE_OUTER_BOUND ( 'NONE', #8145, .T. ) ;
#4917=CONICAL_SURFACE ( 'NONE', #10820, 5.000000000000000888, 1.047197551196596299 ) ;
#4927=ORIENTED_EDGE ( 'NONE', *, *, #643, .F. ) ;
#4928=CONICAL_SURFACE ( 'NONE', #4355, 3.000000000000000000, 0.9599310885968912466 ) ;
#4936=CARTESIAN_POINT ( 'NONE',  ( 3.000000000000000000, 3.673940397442059868E-16, -5.210428571428570521 ) ) ;
#4937=VECTOR ( 'NONE', #3666, 1000.000000000000000 ) ;
#4940=CARTESIAN_POINT ( 'NONE',  ( -2.500000000000000000, 3.061616997868383141E-16, -2.968018054819144158 ) ) ;
#4946=CIRCLE ( 'NONE', #1300, 5.000000000000000888 ) ;
#4949=CARTESIAN_POINT ( 'NONE',  ( 0.000000000000000000, 0.000000000000000000, 0.000000000000000000 ) ) ;
#4950=ORIENTED_EDGE ( 'NONE', *, *, #439, .F. ) ;
#4967=CIRCLE ( 'NONE', #11640, 2.500000000000000000 ) ;
#4968=LINE ( 'NONE', #2322, #10843 ) ;
#4973=DIRECTION ( 'NONE',  ( -0.000000000000000000, -0.000000000000000000, -1.000000000000000000 ) ) ;
#4974=CARTESIAN_POINT ( 'NONE',  ( -2.500000000000005773, -4.330127018922191873, 0.000000000000000000 ) ) ;
#4979=EDGE_CURVE ( 'NONE', #8998, #6548, #7073, .T. ) ;
#4983=CONICAL_SURFACE ( 'NONE', #11653, 3.000000000000000000, 0.9599310885968912466 ) ;
#4991=DIRECTION ( 'NONE',  ( 1.000000000000000000, 0.000000000000000000, 0.000000000000000000 ) ) ;
#4994=EDGE_CURVE ( 'NONE', #7792, #306, #6452, .T. ) ;
#5004=ADVANCED_FACE ( 'NONE', ( #4588 ), #7638, .T. ) ;
#5005=VERTEX_POINT ( 'NONE', #9855 ) ;
#5007=CONICAL_SURFACE ( 'NONE', #8638, 2.500000000000000000, 0.9599310885968755924 ) ;
#5011=AXIS2_PLACEMENT_3D ( 'NONE', #3358, #714, #7980 ) ;
#5012=CONICAL_SURFACE ( 'NONE', #11686, 2.500000000000000000, 0.9599310885968755924 ) ;
#5014=DIRECTION ( 'NONE',  ( -1.000000000000000000, 0.000000000000000000, 0.000000000000000000 ) ) ;
#5024=CARTESIAN_POINT ( 'NONE',  ( 3.000000000000000000, 3.673940397442059868E-16, -1.753742857142857048 ) ) ;
#5035=DIRECTION ( 'NONE',  ( -1.000000000000000000, 0.000000000000000000, 0.000000000000000000 ) ) ;
#5061=CARTESIAN_POINT ( 'NONE',  ( 0.000000000000000000, 0.000000000000000000, -3.996153373752295401 ) ) ;
#5072=CARTESIAN_POINT ( 'NONE',  ( -4.592054218142292754, -3.122278952918454920, -0.3106000600989325400 ) ) ;
#5073=EDGE_CURVE ( 'NONE', #52, #6548, #5433, .T. ) ;
#5091=DIRECTION ( 'NONE',  ( -1.000000000000000000, 0.000000000000000000, 0.000000000000000000 ) ) ;
#5099=CARTESIAN_POINT ( 'NONE',  ( 0.000000000000000000, 0.000000000000000000, -3.482085714285714229 ) ) ;
#5101=AXIS2_PLACEMENT_3D ( 'NONE', #1372, #7783, #5035 ) ;
#5106=ORIENTED_EDGE ( 'NONE', *, *, #6601, .T. ) ;
#5107=AXIS2_PLACEMENT_3D ( 'NONE', #498, #4159, #5014 ) ;
#5111=CARTESIAN_POINT ( 'NONE',  ( 0.000000000000000000, 0.000000000000000000, -0.8895714285714284575 ) ) ;
#5115=LINE ( 'NONE', #1621, #4809 ) ;
#5121=CIRCLE ( 'NONE', #127, 5.000000000000000888 ) ;
#5144=ORIENTED_EDGE ( 'NONE', *, *, #7570, .F. ) ;
#5148=EDGE_CURVE ( 'NONE', #8424, #306, #3998, .T. ) ;
#5152=ORIENTED_EDGE ( 'NONE', *, *, #7542, .F. ) ;
#5155=CARTESIAN_POINT ( 'NONE',  ( -5.000000000000000000, -2.886751345948133540, -6.099999999999999645 ) ) ;
#5159=DIRECTION ( 'NONE',  ( -1.000000000000000000, 0.000000000000000000, 0.000000000000000000 ) ) ;
#5162=AXIS2_PLACEMENT_3D ( 'NONE', #867, #11829, #7360 ) ;
#5184=FACE_OUTER_BOUND ( 'NONE', #10846, .T. ) ;
#5195=VECTOR ( 'NONE', #11554, 1000.000000000000000 ) ;
#5204=CIRCLE ( 'NONE', #1563, 5.000000000000000888 ) ;
#5211=CARTESIAN_POINT ( 'NONE',  ( -3.000000000000000000, 0.000000000000000000, -3.482085714285714229 ) ) ;
#5215=FACE_OUTER_BOUND ( 'NONE', #5374, .T. ) ;
#5219=EDGE_CURVE ( 'NONE', #10233, #1659, #10268, .T. ) ;
#5238=CARTESIAN_POINT ( 'NONE',  ( 5.000000000000000000, 1.947085426416880649, -5.900379292880307602 ) ) ;
#5249=CIRCLE ( 'NONE', #7739, 2.981862520314375153 ) ;
#5266=DIRECTION ( 'NONE',  ( 0.000000000000000000, 0.000000000000000000, 1.000000000000000000 ) ) ;
#5271=DIRECTION ( 'NONE',  ( -0.000000000000000000, -0.000000000000000000, -1.000000000000000000 ) ) ;
#5275=DIRECTION ( 'NONE',  ( -1.000000000000000000, 0.000000000000000000, 0.000000000000000000 ) ) ;
#5278=DIRECTION ( 'NONE',  ( 1.000000000000000000, 0.000000000000000000, 0.000000000000000000 ) ) ;
#5283=LINE ( 'NONE', #11676, #5195 ) ;
#5286=EDGE_CURVE ( 'NONE', #541, #7264, #8789, .T. ) ;
#5288=CARTESIAN_POINT ( 'NONE',  ( 2.074714256722481220, -4.575665857285988736, -6.089444439476605631 ) ) ;
#5289=CIRCLE ( 'NONE', #103, 2.500000000000000000 ) ;
#5291=CARTESIAN_POINT ( 'NONE',  ( 0.000000000000000000, 0.000000000000000000, 0.000000000000000000 ) ) ;
#5298=FACE_OUTER_BOUND ( 'NONE', #9878, .T. ) ;
#5299=DIRECTION ( 'NONE',  ( 1.000000000000000000, 0.000000000000000000, 0.000000000000000000 ) ) ;
#5301=( LENGTH_UNIT ( ) NAMED_UNIT ( * ) SI_UNIT ( .MILLI., .METRE. ) );
#5305=FACE_OUTER_BOUND ( 'NONE', #821, .T. ) ;
#5318=CARTESIAN_POINT ( 'NONE',  ( 2.500000000000000000, 0.000000000000000000, -0.3755037691048591086 ) ) ;
#5323=DIRECTION ( 'NONE',  ( 0.000000000000000000, 0.000000000000000000, 1.000000000000000000 ) ) ;
#5334=DIRECTION ( 'NONE',  ( 1.000000000000000000, 0.000000000000000000, 0.000000000000000000 ) ) ;
#5350=CARTESIAN_POINT ( 'NONE',  ( -1.734723475976807094E-14, -5.773502691896260863, -5.653418012614792154 ) ) ;
#5351=CARTESIAN_POINT ( 'NONE',  ( 0.000000000000000000, 0.000000000000000000, -2.103846626247716234 ) ) ;
#5354=ORIENTED_EDGE ( 'NONE', *, *, #3166, .F. ) ;
#5356=ADVANCED_FACE ( 'NONE', ( #3852 ), #739, .F. ) ;
#5357=DIRECTION ( 'NONE',  ( -1.000000000000000000, 0.000000000000000000, 0.000000000000000000 ) ) ;
#5358=CARTESIAN_POINT ( 'NONE',  ( 0.000000000000000000, 0.000000000000000000, -6.099999999999999645 ) ) ;
#5370=EDGE_CURVE ( 'NONE', #8222, #9107, #11265, .T. ) ;
#5374=EDGE_LOOP ( 'NONE', ( #4639, #10024, #2996, #8819 ) ) ;
#5386=CARTESIAN_POINT ( 'NONE',  ( -4.180704885107416224, -3.359771601077114589, -5.901655677627838159 ) ) ;
#5409=CARTESIAN_POINT ( 'NONE',  ( 1.443735181952764846, -4.939961795957305668, -6.018341802876223667 ) ) ;
#5410=CARTESIAN_POINT ( 'NONE',  ( -2.500000000000000000, 3.061616997868383141E-16, -1.239675197676287643 ) ) ;
#5414=EDGE_CURVE ( 'NONE', #6251, #8998, #9289, .T. ) ;
#5416=CARTESIAN_POINT ( 'NONE',  ( 3.000000000000000000, 3.673940397442059868E-16, -3.482085714285714229 ) ) ;
#5420=DIRECTION ( 'NONE',  ( -0.5000000000000009992, -0.8660254037844380415, 0.000000000000000000 ) ) ;
#5427=ORIENTED_EDGE ( 'NONE', *, *, #6539, .T. ) ;
#5433=LINE ( 'NONE', #4531, #2081 ) ;
#5439=CARTESIAN_POINT ( 'NONE',  ( 5.000000000000000000, -0.9724665692850897880, -6.058069561147904736 ) ) ;
#5441=AXIS2_PLACEMENT_3D ( 'NONE', #11594, #1488, #5091 ) ;
#5453=CARTESIAN_POINT ( 'NONE',  ( 0.000000000000000000, 0.000000000000000000, -0.02539999999999996774 ) ) ;
#5455=FACE_OUTER_BOUND ( 'NONE', #1504, .T. ) ;
#5456=( GEOMETRIC_REPRESENTATION_CONTEXT ( 3 ) GLOBAL_UNCERTAINTY_ASSIGNED_CONTEXT ( ( #7719 ) ) GLOBAL_UNIT_ASSIGNED_CONTEXT ( ( #5301, #2484, #7165 ) ) REPRESENTATION_CONTEXT ( 'NONE', 'WORKASPACE' ) );
#5467=CARTESIAN_POINT ( 'NONE',  ( 1.648146632868998651, 4.821944789745366222, 4.199965926460685847E-15 ) ) ;
#5475=ORIENTED_EDGE ( 'NONE', *, *, #1032, .F. ) ;
#5481=VECTOR ( 'NONE', #1161, 1000.000000000000114 ) ;
#5495=CARTESIAN_POINT ( 'NONE',  ( 0.8179331680533001858, 5.301268757141563093, -5.926062401966624371 ) ) ;
#5498=DIRECTION ( 'NONE',  ( 0.8191520442889913545, 1.003171929053524254E-16, -0.5735764363510468256 ) ) ;
#5501=EDGE_LOOP ( 'NONE', ( #2780, #8519, #11205, #6638, #1607, #7694 ) ) ;
#5507=CARTESIAN_POINT ( 'NONE',  ( 8.673617379884035472E-16, 5.773502691896260863, 0.000000000000000000 ) ) ;
#5511=DIRECTION ( 'NONE',  ( -0.000000000000000000, 0.000000000000000000, -1.000000000000000000 ) ) ;
#5518=ORIENTED_EDGE ( 'NONE', *, *, #10219, .T. ) ;
#5536=ORIENTED_EDGE ( 'NONE', *, *, #6430, .F. ) ;
#5542=AXIS2_PLACEMENT_3D ( 'NONE', #8431, #5746, #3155 ) ;
#5553=AXIS2_PLACEMENT_3D ( 'NONE', #7361, #2624, #5559 ) ;
#5557=CARTESIAN_POINT ( 'NONE',  ( 0.000000000000000000, 0.000000000000000000, -5.210428571428570521 ) ) ;
#5559=DIRECTION ( 'NONE',  ( -1.000000000000000000, 0.000000000000000000, 0.000000000000000000 ) ) ;
#5560=ADVANCED_FACE ( 'NONE', ( #5215 ), #9697, .F. ) ;
#5565=AXIS2_PLACEMENT_3D ( 'NONE', #5061, #8709, #11385 ) ;
#5571=CIRCLE ( 'NONE', #9194, 3.000000000000000000 ) ;
#5576=EDGE_CURVE ( 'NONE', #11822, #3874, #4006, .T. ) ;
#5590=ORIENTED_EDGE ( 'NONE', *, *, #5576, .T. ) ;
#5593=CLOSED_SHELL ( 'NONE', ( #3948, #11193, #11037, #2771, #1430, #9913, #7820, #5356, #7347, #9653, #3810, #11348, #4521, #11055, #5560, #9530, #8223, #4850, #8871, #3719, #7038, #4346, #6935, #10540, #3530, #7844, #10521, #5964, #9227, #11131, #8209, #11419, #10473, #570, #175, #11778, #4553, #9575, #4177, #11455, #7035, #1989, #3431, #3640, #8081, #6244, #3964, #5004, #1446, #3672, #6815, #1333, #710, #273, #8144, #1784, #7382, #10025, #6301, #10382, #10902, #1515, #9303, #2581, #11729, #4418, #558, #8887 ) ) ;
#5595=B_SPLINE_CURVE_WITH_KNOTS ( 'NONE', 3,
 ( #4596, #6351, #868, #11772, #8195, #5386, #8134, #6233 ),
 .UNSPECIFIED., .F., .F.,
 ( 4, 2, 2, 4 ),
 ( 0.002921158011986725936, 0.003648658599403077456, 0.004376159186819428108, 0.005831160361652132015 ),
 .UNSPECIFIED. ) ;
#5602=DIRECTION ( 'NONE',  ( 0.000000000000000000, 0.000000000000000000, 1.000000000000000000 ) ) ;
#5606=ORIENTED_EDGE ( 'NONE', *, *, #2033, .T. ) ;
#5609=LINE ( 'NONE', #9248, #11493 ) ;
#5620=CARTESIAN_POINT ( 'NONE',  ( 2.500000000000005773, 4.330127018922190985, -6.099999999999999645 ) ) ;
#5622=DIRECTION ( 'NONE',  ( 0.000000000000000000, 0.000000000000000000, 1.000000000000000000 ) ) ;
#5623=LINE ( 'NONE', #3256, #10905 ) ;
#5632=CARTESIAN_POINT ( 'NONE',  ( 0.000000000000000000, 0.000000000000000000, -6.099999999999999645 ) ) ;
#5640=ORIENTED_EDGE ( 'NONE', *, *, #2572, .T. ) ;
#5645=CARTESIAN_POINT ( 'NONE',  ( -2.981862520314375153, 3.662834394221259390E-16, -0.01270000000000047133 ) ) ;
#5650=FACE_OUTER_BOUND ( 'NONE', #2730, .T. ) ;
#5667=VECTOR ( 'NONE', #7834, 1000.000000000000114 ) ;
#5672=PLANE ( 'NONE',  #8947 ) ;
#5688=DIRECTION ( 'NONE',  ( -0.8191520442889974607, 0.000000000000000000, -0.5735764363510379438 ) ) ;
#5693=CONICAL_SURFACE ( 'NONE', #10264, 2.500000000000000000, 0.9599310885968755924 ) ;
#5698=LINE ( 'NONE', #100, #9310 ) ;
#5701=ORIENTED_EDGE ( 'NONE', *, *, #2033, .F. ) ;
#5713=VERTEX_POINT ( 'NONE', #505 ) ;
#5715=DIRECTION ( 'NONE',  ( 0.000000000000000000, 0.000000000000000000, 1.000000000000000000 ) ) ;
#5724=ORIENTED_EDGE ( 'NONE', *, *, #10406, .F. ) ;
#5730=CARTESIAN_POINT ( 'NONE',  ( 0.000000000000000000, 0.000000000000000000, -1.403639088038009630 ) ) ;
#5742=CARTESIAN_POINT ( 'NONE',  ( -5.000000000000000888, 0.000000000000000000, 0.000000000000000000 ) ) ;
#5746=DIRECTION ( 'NONE',  ( 0.000000000000000000, 0.000000000000000000, 1.000000000000000000 ) ) ;
#5748=ORIENTED_EDGE ( 'NONE', *, *, #8584, .F. ) ;
#5754=CARTESIAN_POINT ( 'NONE',  ( 0.000000000000000000, 0.000000000000000000, -6.074599999999999334 ) ) ;
#5758=CARTESIAN_POINT ( 'NONE',  ( 0.000000000000000000, 0.000000000000000000, -3.832189483390572970 ) ) ;
#5768=CIRCLE ( 'NONE', #1728, 3.000000000000000000 ) ;
#5771=CIRCLE ( 'NONE', #2513, 5.000000000000000888 ) ;
#5775=CIRCLE ( 'NONE', #7302, 2.500000000000000000 ) ;
#5783=EDGE_CURVE ( 'NONE', #818, #8222, #7766, .T. ) ;
#5795=CARTESIAN_POINT ( 'NONE',  ( -2.500000000000000000, 3.061616997868383141E-16, -4.860324802323723326 ) ) ;
#5798=VERTEX_POINT ( 'NONE', #5024 ) ;
#5809=ORIENTED_EDGE ( 'NONE', *, *, #10689, .F. ) ;
#5818=DIRECTION ( 'NONE',  ( -0.000000000000000000, -0.000000000000000000, -1.000000000000000000 ) ) ;
#5821=LINE ( 'NONE', #9272, #1656 ) ;
#5831=DIRECTION ( 'NONE',  ( -0.8660254037844380415, 0.5000000000000009992, 0.000000000000000000 ) ) ;
#5840=VERTEX_POINT ( 'NONE', #5918 ) ;
#5846=B_SPLINE_CURVE_WITH_KNOTS ( 'NONE', 3,
 ( #11491, #11611, #8816, #10712, #9648, #7919, #1613, #8192 ),
 .UNSPECIFIED., .F., .F.,
 ( 4, 2, 2, 4 ),
 ( 0.002921158011986720298, 0.003648658599403072252, 0.004376159186819423771, 0.005831160361652126811 ),
 .UNSPECIFIED. ) ;
#5856=CONICAL_SURFACE ( 'NONE', #2395, 3.000000000000000888, 0.9599310885968804774 ) ;
#5863=DIRECTION ( 'NONE',  ( -0.8191520442889885789, 1.003171929053520802E-16, 0.5735764363510507113 ) ) ;
#5868=VECTOR ( 'NONE', #10519, 1000.000000000000000 ) ;
#5890=CONICAL_SURFACE ( 'NONE', #9705, 3.000000000000000000, 0.9599310885968912466 ) ;
#5893=CONICAL_SURFACE ( 'NONE', #10838, 3.000000000000000000, 0.9599310885968912466 ) ;
#5898=DIRECTION ( 'NONE',  ( -1.000000000000000000, 0.000000000000000000, 0.000000000000000000 ) ) ;
#5903=ORIENTED_EDGE ( 'NONE', *, *, #2212, .F. ) ;
#5918=CARTESIAN_POINT ( 'NONE',  ( -2.500000000000000000, 3.061616997868383141E-16, -5.724496230895143256 ) ) ;
#5923=AXIS2_PLACEMENT_3D ( 'NONE', #2677, #1591, #7298 ) ;
#5928=CONICAL_SURFACE ( 'NONE', #1325, 2.450000000000000178, 0.9599310885968801443 ) ;
#5943=DIRECTION ( 'NONE',  ( -1.000000000000000000, 0.000000000000000000, 0.000000000000000000 ) ) ;
#5944=CONICAL_SURFACE ( 'NONE', #9561, 2.500000000000000000, 0.9599310885968755924 ) ;
#5947=CIRCLE ( 'NONE', #9565, 5.000000000000000888 ) ;
#5951=CARTESIAN_POINT ( 'NONE',  ( 0.000000000000000000, 0.000000000000000000, -3.482085714285714229 ) ) ;
#5964=ADVANCED_FACE ( 'NONE', ( #243 ), #7627, .F. ) ;
#5966=DIRECTION ( 'NONE',  ( -0.000000000000000000, 0.000000000000000000, -1.000000000000000000 ) ) ;
#5975=FACE_OUTER_BOUND ( 'NONE', #6897, .T. ) ;
#5976=CARTESIAN_POINT ( 'NONE',  ( 0.000000000000000000, 0.000000000000000000, -6.099999999999999645 ) ) ;
#5977=CONICAL_SURFACE ( 'NONE', #9021, 2.500000000000000000, 0.9599310885968755924 ) ;
#5981=ORIENTED_EDGE ( 'NONE', *, *, #11024, .F. ) ;
#5989=CARTESIAN_POINT ( 'NONE',  ( 2.500000000000000000, 0.000000000000000000, -5.724496230895143256 ) ) ;
#5993=CARTESIAN_POINT ( 'NONE',  ( -2.500000000000000000, 3.061616997868383141E-16, -3.996153373752295401 ) ) ;
#5994=DIRECTION ( 'NONE',  ( 0.8191520442889974607, 1.003171929053531649E-16, -0.5735764363510379438 ) ) ;
#5996=VERTEX_POINT ( 'NONE', #9596 ) ;
#6013=ORIENTED_EDGE ( 'NONE', *, *, #4258, .T. ) ;
#6021=FACE_OUTER_BOUND ( 'NONE', #4484, .T. ) ;
#6025=ORIENTED_EDGE ( 'NONE', *, *, #10309, .F. ) ;
#6032=SHAPE_REPRESENTATION_RELATIONSHIP ( 'NONE' , 'NONE' ,  #9454, #6721 ) ;
#6042=MECHANICAL_DESIGN_GEOMETRIC_PRESENTATION_REPRESENTATION('',(#11181),#5456);
#6055=LINE ( 'NONE', #8739, #4664 ) ;
#6067=CARTESIAN_POINT ( 'NONE',  ( -5.000000000000000000, 2.886751345948126879, -0.4465819873852047150 ) ) ;
#6069=CONICAL_SURFACE ( 'NONE', #3953, 2.500000000000000000, 0.9599310885968755924 ) ;
#6080=FACE_OUTER_BOUND ( 'NONE', #9415, .T. ) ;
#6100=AXIS2_PLACEMENT_3D ( 'NONE', #11253, #10366, #4679 ) ;
#6101=EDGE_CURVE ( 'NONE', #7933, #3923, #1718, .T. ) ;
#6105=CARTESIAN_POINT ( 'NONE',  ( 0.000000000000000000, 0.000000000000000000, -6.099999999999999645 ) ) ;
#6120=VECTOR ( 'NONE', #2382, 1000.000000000000000 ) ;
#6125=LINE ( 'NONE', #11430, #4169 ) ;
#6137=CARTESIAN_POINT ( 'NONE',  ( -5.000000000000000000, 2.886751345948134428, -5.653418012614792154 ) ) ;
#6138=AXIS2_PLACEMENT_3D ( 'NONE', #8036, #3484, #11674 ) ;
#6148=CARTESIAN_POINT ( 'NONE',  ( 0.000000000000000000, 0.000000000000000000, -6.099999999999999645 ) ) ;
#6149=AXIS2_PLACEMENT_3D ( 'NONE', #1801, #1084, #900 ) ;
#6152=VECTOR ( 'NONE', #3766, 1000.000000000000000 ) ;
#6160=AXIS2_PLACEMENT_3D ( 'NONE', #1200, #9468, #9406 ) ;
#6164=CARTESIAN_POINT ( 'NONE',  ( 0.000000000000000000, 0.000000000000000000, 0.000000000000000000 ) ) ;
#6174=CARTESIAN_POINT ( 'NONE',  ( 0.000000000000000000, 0.000000000000000000, -6.074599999999999334 ) ) ;
#6183=ORIENTED_EDGE ( 'NONE', *, *, #6744, .F. ) ;
#6199=CARTESIAN_POINT ( 'NONE',  ( 0.4079457818577022499, -5.537975084925951919, -5.789399939901062275 ) ) ;
#6217=ORIENTED_EDGE ( 'NONE', *, *, #2426, .F. ) ;
#6221=B_SPLINE_CURVE_WITH_KNOTS ( 'NONE', 3,
 ( #11550, #10152, #991, #6402, #11828, #3694 ),
 .UNSPECIFIED., .F., .F.,
 ( 4, 2, 4 ),
 ( 0.005150343764683554260, 0.006610526168996385711, 0.008070708573309217163 ),
 .UNSPECIFIED. ) ;
#6223=DIRECTION ( 'NONE',  ( -0.000000000000000000, -0.000000000000000000, -1.000000000000000000 ) ) ;
#6225=CARTESIAN_POINT ( 'NONE',  ( 3.000000000000000000, 3.673940397442059868E-16, -0.02539999999999996774 ) ) ;
#6230=B_SPLINE_CURVE_WITH_KNOTS ( 'NONE', 3,
 ( #811, #3750, #4480, #5439, #9087, #10870 ),
 .UNSPECIFIED., .F., .F.,
 ( 4, 2, 4 ),
 ( 0.005150343764683554260, 0.006610526168996384844, 0.008070708573309215428 ),
 .UNSPECIFIED. ) ;
#6233=CARTESIAN_POINT ( 'NONE',  ( -5.000000000000000000, -2.886751345948134428, -5.653418012614792154 ) ) ;
#6237=CARTESIAN_POINT ( 'NONE',  ( -3.000000000000000000, 0.000000000000000000, -0.8895714285714284575 ) ) ;
#6244=ADVANCED_FACE ( 'NONE', ( #11435 ), #11273, .T. ) ;
#6250=CARTESIAN_POINT ( 'NONE',  ( -3.000000000000000888, 3.673940397442060854E-16, -6.099999999999997868 ) ) ;
#6251=VERTEX_POINT ( 'NONE', #6250 ) ;
#6252=LINE ( 'NONE', #4322, #11483 ) ;
#6253=ORIENTED_EDGE ( 'NONE', *, *, #7338, .F. ) ;
#6260=CARTESIAN_POINT ( 'NONE',  ( 4.182066831946701591, -3.358985280702831755, -5.926062401966622595 ) ) ;
#6266=CARTESIAN_POINT ( 'NONE',  ( 0.000000000000000000, 0.000000000000000000, -6.099999999999999645 ) ) ;
#6269=DIRECTION ( 'NONE',  ( 1.000000000000000000, 0.000000000000000000, 0.000000000000000000 ) ) ;
#6286=EDGE_LOOP ( 'NONE', ( #448, #971, #7179, #6253 ) ) ;
#6290=DIRECTION ( 'NONE',  ( -0.000000000000000000, -0.000000000000000000, 1.000000000000000000 ) ) ;
#6299=LINE ( 'NONE', #6471, #6931 ) ;
#6301=ADVANCED_FACE ( 'NONE', ( #5455 ), #4983, .F. ) ;
#6316=CIRCLE ( 'NONE', #3426, 3.000000000000000000 ) ;
#6325=DIRECTION ( 'NONE',  ( -1.000000000000000000, 0.000000000000000000, 0.000000000000000000 ) ) ;
#6331=CARTESIAN_POINT ( 'NONE',  ( -5.000000000000000000, -2.886751345948133540, -6.099999999999999645 ) ) ;
#6346=VECTOR ( 'NONE', #3522, 1000.000000000000000 ) ;
#6351=CARTESIAN_POINT ( 'NONE',  ( -2.712167343862823987, -4.207632145829752979, -6.099999999999999645 ) ) ;
#6353=DIRECTION ( 'NONE',  ( -1.000000000000000000, 0.000000000000000000, 0.000000000000000000 ) ) ;
#6356=ORIENTED_EDGE ( 'NONE', *, *, #10786, .F. ) ;
#6359=CARTESIAN_POINT ( 'NONE',  ( -5.000000000000000000, 2.886751345948126879, -6.099999999999999645 ) ) ;
#6361=EDGE_LOOP ( 'NONE', ( #10492, #10043, #4727, #455 ) ) ;
#6362=EDGE_CURVE ( 'NONE', #541, #10278, #5947, .T. ) ;
#6375=LINE ( 'NONE', #10841, #2619 ) ;
#6383=FACE_OUTER_BOUND ( 'NONE', #7981, .T. ) ;
#6384=VERTEX_POINT ( 'NONE', #1721 ) ;
#6391=EDGE_LOOP ( 'NONE', ( #281, #9197, #5981, #7424, #9340, #10052 ) ) ;
#6402=CARTESIAN_POINT ( 'NONE',  ( 5.000000000000000000, -0.9724665692850895660, -0.04193043885209624122 ) ) ;
#6410=PLANE ( 'NONE',  #6449 ) ;
#6412=EDGE_CURVE ( 'NONE', #10937, #8985, #180, .T. ) ;
#6413=FACE_OUTER_BOUND ( 'NONE', #11490, .T. ) ;
#6415=FACE_OUTER_BOUND ( 'NONE', #713, .T. ) ;
#6420=ORIENTED_EDGE ( 'NONE', *, *, #10682, .T. ) ;
#6427=AXIS2_PLACEMENT_3D ( 'NONE', #10906, #724, #9060 ) ;
#6430=EDGE_CURVE ( 'NONE', #8424, #11218, #1775, .T. ) ;
#6445=AXIS2_PLACEMENT_3D ( 'NONE', #4949, #8605, #7705 ) ;
#6449=AXIS2_PLACEMENT_3D ( 'NONE', #5507, #9329, #10042 ) ;
#6451=VERTEX_POINT ( 'NONE', #2746 ) ;
#6452=LINE ( 'NONE', #4420, #4196 ) ;
#6455=VERTEX_POINT ( 'NONE', #3697 ) ;
#6456=EDGE_CURVE ( 'NONE', #1322, #11030, #378, .T. ) ;
#6462=DIRECTION ( 'NONE',  ( -1.000000000000000000, 0.000000000000000000, 0.000000000000000000 ) ) ;
#6471=CARTESIAN_POINT ( 'NONE',  ( -2.500000000000000000, 3.061616997868383141E-16, -6.099999999999999645 ) ) ;
#6502=LINE ( 'NONE', #8409, #1535 ) ;
#6503=EDGE_LOOP ( 'NONE', ( #3186, #8786, #9567, #6776 ) ) ;
#6508=VECTOR ( 'NONE', #6879, 1000.000000000000000 ) ;
#6514=ORIENTED_EDGE ( 'NONE', *, *, #2950, .T. ) ;
#6527=LINE ( 'NONE', #933, #6346 ) ;
#6539=EDGE_CURVE ( 'NONE', #364, #3733, #5595, .T. ) ;
#6541=CARTESIAN_POINT ( 'NONE',  ( -4.182066831946702479, 3.358985280702821985, -0.1739375980333739413 ) ) ;
#6547=CIRCLE ( 'NONE', #2131, 3.000000000000000000 ) ;
#6548=VERTEX_POINT ( 'NONE', #1658 ) ;
#6549=CARTESIAN_POINT ( 'NONE',  ( 2.500000000000000000, 0.000000000000000000, -0.5394676594665810399 ) ) ;
#6551=EDGE_CURVE ( 'NONE', #7792, #8673, #8430, .T. ) ;
#6553=CARTESIAN_POINT ( 'NONE',  ( 0.000000000000000000, 0.000000000000000000, -0.3755037691048591086 ) ) ;
#6566=CARTESIAN_POINT ( 'NONE',  ( -5.000000000000000000, 2.419979747126329794, -5.788163366729714099 ) ) ;
#6587=LINE ( 'NONE', #3037, #7089 ) ;
#6594=LINE ( 'NONE', #4783, #4238 ) ;
#6601=EDGE_CURVE ( 'NONE', #6455, #6801, #5623, .T. ) ;
#6608=VERTEX_POINT ( 'NONE', #11163 ) ;
#6615=LINE ( 'NONE', #10189, #8984 ) ;
#6627=EDGE_LOOP ( 'NONE', ( #11642, #6356, #1353, #2631 ) ) ;
#6635=DIRECTION ( 'NONE',  ( -0.000000000000000000, -0.000000000000000000, 1.000000000000000000 ) ) ;
#6638=ORIENTED_EDGE ( 'NONE', *, *, #4103, .F. ) ;
#6650=DIRECTION ( 'NONE',  ( 0.000000000000000000, 0.000000000000000000, 1.000000000000000000 ) ) ;
#6651=AXIS2_PLACEMENT_3D ( 'NONE', #5754, #2928, #2752 ) ;
#6657=CARTESIAN_POINT ( 'NONE',  ( -1.734723475976807094E-14, -5.773502691896260863, -0.4465819873852071575 ) ) ;
#6658=CARTESIAN_POINT ( 'NONE',  ( -5.000000000000000000, 2.886751345948126879, -0.4465819873852047150 ) ) ;
#6663=ORIENTED_EDGE ( 'NONE', *, *, #776, .T. ) ;
#6674=CYLINDRICAL_SURFACE ( 'NONE', #2640, 2.500000000000000000 ) ;
#6683=CARTESIAN_POINT ( 'NONE',  ( 2.500000000000000000, 0.000000000000000000, -4.860324802323723326 ) ) ;
#6701=ORIENTED_EDGE ( 'NONE', *, *, #11407, .T. ) ;
#6715=CARTESIAN_POINT ( 'NONE',  ( -1.734723475976807094E-14, -5.773502691896260863, -5.653418012614792154 ) ) ;
#6719=DIRECTION ( 'NONE',  ( -1.000000000000000000, 0.000000000000000000, 0.000000000000000000 ) ) ;
#6721=ADVANCED_BREP_SHAPE_REPRESENTATION ( '', ( #4897, #4738 ), #10420 ) ;
#6737=CIRCLE ( 'NONE', #8642, 2.500000000000000000 ) ;
#6739=CARTESIAN_POINT ( 'NONE',  ( 0.000000000000000000, 0.000000000000000000, -6.099999999999999645 ) ) ;
#6741=ORIENTED_EDGE ( 'NONE', *, *, #1072, .F. ) ;
#6743=FACE_OUTER_BOUND ( 'NONE', #3067, .T. ) ;
#6744=EDGE_CURVE ( 'NONE', #66, #1659, #5768, .T. ) ;
#6745=AXIS2_PLACEMENT_3D ( 'NONE', #1000, #8260, #1836 ) ;
#6751=ORIENTED_EDGE ( 'NONE', *, *, #190, .T. ) ;
#6758=ORIENTED_EDGE ( 'NONE', *, *, #4777, .T. ) ;
#6768=UNCERTAINTY_MEASURE_WITH_UNIT (LENGTH_MEASURE( 1.000000000000000082E-05 ), #11276, 'distance_accuracy_value', 'NONE');
#6770=EDGE_CURVE ( 'NONE', #11030, #9242, #123, .T. ) ;
#6776=ORIENTED_EDGE ( 'NONE', *, *, #4299, .F. ) ;
#6793=ORIENTED_EDGE ( 'NONE', *, *, #4103, .T. ) ;
#6798=B_SPLINE_CURVE_WITH_KNOTS ( 'NONE', 3,
 ( #7984, #3424, #5288, #2713, #5409, #4568, #6199, #5350 ),
 .UNSPECIFIED., .F., .F.,
 ( 4, 2, 2, 4 ),
 ( 0.002921158011986708155, 0.003648658599403066180, 0.004376159186819424639, 0.005831160361652140689 ),
 .UNSPECIFIED. ) ;
#6801=VERTEX_POINT ( 'NONE', #3432 ) ;
#6815=ADVANCED_FACE ( 'NONE', ( #5298 ), #8846, .T. ) ;
#6832=CARTESIAN_POINT ( 'NONE',  ( 0.000000000000000000, 0.000000000000000000, -3.482085714285714229 ) ) ;
#6850=CARTESIAN_POINT ( 'NONE',  ( 0.000000000000000000, 0.000000000000000000, -4.696360911962001339 ) ) ;
#6851=DIRECTION ( 'NONE',  ( -0.000000000000000000, -0.000000000000000000, -1.000000000000000000 ) ) ;
#6858=VECTOR ( 'NONE', #7436, 1000.000000000000114 ) ;
#6862=CARTESIAN_POINT ( 'NONE',  ( 0.000000000000000000, 0.000000000000000000, -5.560532340533429263 ) ) ;
#6879=DIRECTION ( 'NONE',  ( 0.8191520442889885789, 0.000000000000000000, 0.5735764363510507113 ) ) ;
#6890=VERTEX_POINT ( 'NONE', #786 ) ;
#6897=EDGE_LOOP ( 'NONE', ( #7706, #23, #3599, #209 ) ) ;
#6902=AXIS2_PLACEMENT_3D ( 'NONE', #4483, #3519, #9863 ) ;
#6908=ORIENTED_EDGE ( 'NONE', *, *, #10668, .F. ) ;
#6920=PRODUCT_DEFINITION_SHAPE ( 'NONE', 'NONE',  #3298 ) ;
#6923=CONICAL_SURFACE ( 'NONE', #5011, 2.500000000000000000, 0.9599310885968755924 ) ;
#6931=VECTOR ( 'NONE', #3479, 1000.000000000000000 ) ;
#6932=CYLINDRICAL_SURFACE ( 'NONE', #1462, 2.500000000000000000 ) ;
#6933=EDGE_LOOP ( 'NONE', ( #5809, #9630, #5903 ) ) ;
#6935=ADVANCED_FACE ( 'NONE', ( #551 ), #4216, .F. ) ;
#6954=CARTESIAN_POINT ( 'NONE',  ( 0.8192951148925836646, -5.300482436767290473, -0.1983443223721653714 ) ) ;
#6958=ORIENTED_EDGE ( 'NONE', *, *, #11325, .F. ) ;
#6974=ORIENTED_EDGE ( 'NONE', *, *, #7835, .F. ) ;
#6986=CARTESIAN_POINT ( 'NONE',  ( 0.000000000000000000, 0.000000000000000000, -0.02539999999999996774 ) ) ;
#6998=ORIENTED_EDGE ( 'NONE', *, *, #3208, .T. ) ;
#7006=ORIENTED_EDGE ( 'NONE', *, *, #776, .F. ) ;
#7010=CARTESIAN_POINT ( 'NONE',  ( 0.000000000000000000, 0.000000000000000000, 0.000000000000000000 ) ) ;
#7031=VECTOR ( 'NONE', #4453, 1000.000000000000000 ) ;
#7033=PRODUCT_DEFINITION_CONTEXT ( 'detailed design', #20, 'design' ) ;
#7035=ADVANCED_FACE ( 'NONE', ( #4630 ), #2722, .T. ) ;
#7038=ADVANCED_FACE ( 'NONE', ( #5650 ), #10245, .F. ) ;
#7039=CARTESIAN_POINT ( 'NONE',  ( -0.4079457818577095773, 5.537975084925940372, -0.3106000600989312077 ) ) ;
#7047=CARTESIAN_POINT ( 'NONE',  ( -5.000000000000000888, 0.9828435001097601820, -0.04309034703445699388 ) ) ;
#7048=DIRECTION ( 'NONE',  ( -1.000000000000000000, 0.000000000000000000, 0.000000000000000000 ) ) ;
#7052=DIRECTION ( 'NONE',  ( 0.000000000000000000, 0.000000000000000000, 1.000000000000000000 ) ) ;
#7066=DIRECTION ( 'NONE',  ( -1.000000000000000000, 0.000000000000000000, 0.000000000000000000 ) ) ;
#7073=CIRCLE ( 'NONE', #9546, 3.000000000000000888 ) ;
#7076=ORIENTED_EDGE ( 'NONE', *, *, #7774, .T. ) ;
#7089=VECTOR ( 'NONE', #5863, 1000.000000000000000 ) ;
#7093=VERTEX_POINT ( 'NONE', #964 ) ;
#7097=CARTESIAN_POINT ( 'NONE',  ( 8.673617379884035472E-16, 5.773502691896260863, -6.099999999999999645 ) ) ;
#7100=LINE ( 'NONE', #5410, #4937 ) ;
#7112=DIRECTION ( 'NONE',  ( -0.000000000000000000, -0.000000000000000000, -1.000000000000000000 ) ) ;
#7115=ORIENTED_EDGE ( 'NONE', *, *, #7197, .F. ) ;
#7127=DIRECTION ( 'NONE',  ( -1.000000000000000000, 0.000000000000000000, 0.000000000000000000 ) ) ;
#7134=FACE_OUTER_BOUND ( 'NONE', #4017, .T. ) ;
#7151=CARTESIAN_POINT ( 'NONE',  ( 0.000000000000000000, 5.773502691896260863, -0.4465819873852071575 ) ) ;
#7155=DIRECTION ( 'NONE',  ( -1.000000000000000000, 0.000000000000000000, 0.000000000000000000 ) ) ;
#7163=CARTESIAN_POINT ( 'NONE',  ( 0.000000000000000000, 0.000000000000000000, -2.617914285714285416 ) ) ;
#7165=( NAMED_UNIT ( * ) SI_UNIT ( $, .STERADIAN. ) SOLID_ANGLE_UNIT ( ) );
#7179=ORIENTED_EDGE ( 'NONE', *, *, #11407, .F. ) ;
#7180=DIRECTION ( 'NONE',  ( -1.000000000000000000, 0.000000000000000000, 0.000000000000000000 ) ) ;
#7197=EDGE_CURVE ( 'NONE', #1659, #66, #3659, .T. ) ;
#7212=ORIENTED_EDGE ( 'NONE', *, *, #4525, .T. ) ;
#7229=ORIENTED_EDGE ( 'NONE', *, *, #4691, .F. ) ;
#7251=ORIENTED_EDGE ( 'NONE', *, *, #8182, .F. ) ;
#7255=VECTOR ( 'NONE', #822, 1000.000000000000000 ) ;
#7260=DIRECTION ( 'NONE',  ( -1.000000000000000000, 0.000000000000000000, 0.000000000000000000 ) ) ;
#7261=FACE_OUTER_BOUND ( 'NONE', #9892, .T. ) ;
#7264=VERTEX_POINT ( 'NONE', #7151 ) ;
#7298=DIRECTION ( 'NONE',  ( -1.000000000000000000, 0.000000000000000000, 0.000000000000000000 ) ) ;
#7302=AXIS2_PLACEMENT_3D ( 'NONE', #4865, #3902, #1254 ) ;
#7305=CARTESIAN_POINT ( 'NONE',  ( 0.000000000000000000, 0.000000000000000000, -6.074599999999999334 ) ) ;
#7306=CARTESIAN_POINT ( 'NONE',  ( 3.000000000000000888, 3.673940397442060854E-16, -6.074599999999999334 ) ) ;
#7307=DIRECTION ( 'NONE',  ( -1.000000000000000000, 0.000000000000000000, 0.000000000000000000 ) ) ;
#7309=DIRECTION ( 'NONE',  ( -0.000000000000000000, -0.000000000000000000, -1.000000000000000000 ) ) ;
#7312=CONICAL_SURFACE ( 'NONE', #222, 5.000000000000000888, 1.047197551196596299 ) ;
#7317=CARTESIAN_POINT ( 'NONE',  ( -2.500000000000000000, 3.061616997868383141E-16, -5.560532340533429263 ) ) ;
#7328=EDGE_CURVE ( 'NONE', #9312, #7933, #6252, .T. ) ;
#7338=EDGE_CURVE ( 'NONE', #2315, #818, #5283, .T. ) ;
#7344=VERTEX_POINT ( 'NONE', #9709 ) ;
#7347=ADVANCED_FACE ( 'NONE', ( #9880 ), #6923, .F. ) ;
#7348=ORIENTED_EDGE ( 'NONE', *, *, #931, .F. ) ;
#7353=DIRECTION ( 'NONE',  ( -0.000000000000000000, -0.000000000000000000, 1.000000000000000000 ) ) ;
#7358=CARTESIAN_POINT ( 'NONE',  ( -5.000000000000000000, 2.886751345948134428, -5.653418012614792154 ) ) ;
#7360=DIRECTION ( 'NONE',  ( -1.000000000000000000, 0.000000000000000000, 0.000000000000000000 ) ) ;
#7361=CARTESIAN_POINT ( 'NONE',  ( 0.000000000000000000, 0.000000000000000000, 0.000000000000000000 ) ) ;
#7371=DIRECTION ( 'NONE',  ( -1.000000000000000000, 0.000000000000000000, 0.000000000000000000 ) ) ;
#7377=ORIENTED_EDGE ( 'NONE', *, *, #10786, .T. ) ;
#7380=B_SPLINE_CURVE_WITH_KNOTS ( 'NONE', 3,
 ( #11534, #521, #1598, #3284, #695, #6954, #3467, #1543 ),
 .UNSPECIFIED., .F., .F.,
 ( 4, 2, 2, 4 ),
 ( 0.002921158011986708155, 0.003648658599403066180, 0.004376159186819424639, 0.005831160361652140689 ),
 .UNSPECIFIED. ) ;
#7382=ADVANCED_FACE ( 'NONE', ( #1505 ), #9775, .F. ) ;
#7384=FACE_OUTER_BOUND ( 'NONE', #4211, .T. ) ;
#7406=VECTOR ( 'NONE', #9713, 1000.000000000000114 ) ;
#7415=VECTOR ( 'NONE', #2558, 1000.000000000000114 ) ;
#7418=CARTESIAN_POINT ( 'NONE',  ( 0.000000000000000000, 0.000000000000000000, -4.346257142857142597 ) ) ;
#7424=ORIENTED_EDGE ( 'NONE', *, *, #4555, .F. ) ;
#7428=LINE ( 'NONE', #2863, #11258 ) ;
#7434=DIRECTION ( 'NONE',  ( -0.000000000000000000, -0.000000000000000000, 1.000000000000000000 ) ) ;
#7436=DIRECTION ( 'NONE',  ( 0.8191520442889974607, 1.003171929053531649E-16, -0.5735764363510379438 ) ) ;
#7439=AXIS2_PLACEMENT_3D ( 'NONE', #5351, #9003, #3546 ) ;
#7450=ORIENTED_EDGE ( 'NONE', *, *, #8952, .T. ) ;
#7460=CARTESIAN_POINT ( 'NONE',  ( -5.000000000000000888, 0.9828435001097621804, -6.056909652965543067 ) ) ;
#7461=VECTOR ( 'NONE', #2336, 1000.000000000000000 ) ;
#7464=CARTESIAN_POINT ( 'NONE',  ( -5.000000000000000000, -0.9724665692850886778, -6.058069561147902959 ) ) ;
#7465=LINE ( 'NONE', #4638, #386 ) ;
#7485=CARTESIAN_POINT ( 'NONE',  ( 0.000000000000000000, 0.000000000000000000, -4.860324802323723326 ) ) ;
#7497=CARTESIAN_POINT ( 'NONE',  ( 2.500000000000000000, 0.000000000000000000, -6.099999999999999645 ) ) ;
#7498=CARTESIAN_POINT ( 'NONE',  ( -5.000000000000000000, 0.000000000000000000, -6.099999999999999645 ) ) ;
#7510=DIRECTION ( 'NONE',  ( 0.000000000000000000, 0.000000000000000000, 1.000000000000000000 ) ) ;
#7513=ORIENTED_EDGE ( 'NONE', *, *, #4979, .F. ) ;
#7522=CARTESIAN_POINT ( 'NONE',  ( -5.000000000000000000, 0.000000000000000000, -6.099999999999999645 ) ) ;
#7542=EDGE_CURVE ( 'NONE', #8959, #11839, #6527, .T. ) ;
#7546=CARTESIAN_POINT ( 'NONE',  ( 0.000000000000000000, 0.000000000000000000, -1.239675197676287643 ) ) ;
#7554=CARTESIAN_POINT ( 'NONE',  ( -0.8179331680533127313, -5.301268757141564869, -0.1739375980333775218 ) ) ;
#7555=LINE ( 'NONE', #3893, #6858 ) ;
#7558=ORIENTED_EDGE ( 'NONE', *, *, #7197, .T. ) ;
#7568=CYLINDRICAL_SURFACE ( 'NONE', #2257, 2.500000000000000000 ) ;
#7569=ORIENTED_EDGE ( 'NONE', *, *, #6412, .F. ) ;
#7570=EDGE_CURVE ( 'NONE', #8673, #7792, #1929, .T. ) ;
#7587=DIRECTION ( 'NONE',  ( 1.000000000000000000, 0.000000000000000000, 0.000000000000000000 ) ) ;
#7588=ORIENTED_EDGE ( 'NONE', *, *, #4490, .F. ) ;
#7608=ORIENTED_EDGE ( 'NONE', *, *, #3901, .F. ) ;
#7612=FACE_OUTER_BOUND ( 'NONE', #9637, .T. ) ;
#7621=CYLINDRICAL_SURFACE ( 'NONE', #2321, 2.500000000000000000 ) ;
#7627=CYLINDRICAL_SURFACE ( 'NONE', #9940, 2.500000000000000000 ) ;
#7635=CARTESIAN_POINT ( 'NONE',  ( -4.999999999999999112, -2.417244626924487605, -5.788952927922133007 ) ) ;
#7638=CONICAL_SURFACE ( 'NONE', #5923, 5.000000000000000888, 1.047197551196596299 ) ;
#7647=ORIENTED_EDGE ( 'NONE', *, *, #5286, .F. ) ;
#7661=LINE ( 'NONE', #398, #9285 ) ;
#7680=FACE_OUTER_BOUND ( 'NONE', #6627, .T. ) ;
#7690=CARTESIAN_POINT ( 'NONE',  ( 0.000000000000000000, 0.000000000000000000, 0.000000000000000000 ) ) ;
#7694=ORIENTED_EDGE ( 'NONE', *, *, #10219, .F. ) ;
#7700=EDGE_CURVE ( 'NONE', #6451, #6801, #8057, .T. ) ;
#7705=DIRECTION ( 'NONE',  ( -1.000000000000000000, 0.000000000000000000, 0.000000000000000000 ) ) ;
#7706=ORIENTED_EDGE ( 'NONE', *, *, #9937, .F. ) ;
#7708=CARTESIAN_POINT ( 'NONE',  ( -2.500000000000003553, 4.330127018922192761, 0.000000000000000000 ) ) ;
#7719=UNCERTAINTY_MEASURE_WITH_UNIT (LENGTH_MEASURE( 1.000000000000000082E-05 ), #5301, 'distance_accuracy_value', 'NONE');
#7739=AXIS2_PLACEMENT_3D ( 'NONE', #3168, #7784, #8447 ) ;
#7742=EDGE_LOOP ( 'NONE', ( #7588, #2166, #8203, #2170 ) ) ;
#7751=CARTESIAN_POINT ( 'NONE',  ( -2.074714256722480332, 4.575665857285978966, -6.089444439476609183 ) ) ;
#7760=B_SPLINE_CURVE_WITH_KNOTS ( 'NONE', 3,
 ( #2872, #9777, #1573, #5238, #8885, #3427 ),
 .UNSPECIFIED., .F., .F.,
 ( 4, 2, 4 ),
 ( 0.008070708573309215428, 0.009531758523483287518, 0.01099280847365735961 ),
 .UNSPECIFIED. ) ;
#7766=LINE ( 'NONE', #4167, #6508 ) ;
#7771=ORIENTED_EDGE ( 'NONE', *, *, #10482, .F. ) ;
#7774=EDGE_CURVE ( 'NONE', #5996, #7952, #2312, .T. ) ;
#7781=VECTOR ( 'NONE', #4035, 1000.000000000000114 ) ;
#7783=DIRECTION ( 'NONE',  ( -0.000000000000000000, -0.000000000000000000, -1.000000000000000000 ) ) ;
#7784=DIRECTION ( 'NONE',  ( 0.000000000000000000, 0.000000000000000000, 1.000000000000000000 ) ) ;
#7792=VERTEX_POINT ( 'NONE', #5795 ) ;
#7804=ORIENTED_EDGE ( 'NONE', *, *, #3458, .F. ) ;
#7812=CARTESIAN_POINT ( 'NONE',  ( -0.8192951148925881055, 5.300482436767277150, -5.901655677627839935 ) ) ;
#7818=( NAMED_UNIT ( * ) SI_UNIT ( $, .STERADIAN. ) SOLID_ANGLE_UNIT ( ) );
#7820=ADVANCED_FACE ( 'NONE', ( #1940 ), #5977, .F. ) ;
#7832=VERTEX_POINT ( 'NONE', #8535 ) ;
#7834=DIRECTION ( 'NONE',  ( 0.8191520442889974607, 1.003171929053531649E-16, -0.5735764363510379438 ) ) ;
#7835=EDGE_CURVE ( 'NONE', #1507, #11839, #9986, .T. ) ;
#7841=ORIENTED_EDGE ( 'NONE', *, *, #9045, .F. ) ;
#7844=ADVANCED_FACE ( 'NONE', ( #11274 ), #3085, .F. ) ;
#7858=CARTESIAN_POINT ( 'NONE',  ( 0.000000000000000000, 0.000000000000000000, 0.000000000000000000 ) ) ;
#7867=ORIENTED_EDGE ( 'NONE', *, *, #4051, .T. ) ;
#7871=LINE ( 'NONE', #3312, #7781 ) ;
#7874=AXIS2_PLACEMENT_3D ( 'NONE', #11832, #7309, #9149 ) ;
#7875=AXIS2_PLACEMENT_3D ( 'NONE', #7097, #10779, #9228 ) ;
#7879=CARTESIAN_POINT ( 'NONE',  ( 0.000000000000000000, 0.000000000000000000, -6.099999999999999645 ) ) ;
#7884=DIRECTION ( 'NONE',  ( 0.000000000000000000, 0.000000000000000000, 1.000000000000000000 ) ) ;
#7886=CARTESIAN_POINT ( 'NONE',  ( -3.556264818047240706, -3.720292241887095397, -0.08165819712377302142 ) ) ;
#7888=ORIENTED_EDGE ( 'NONE', *, *, #8182, .T. ) ;
#7901=EDGE_LOOP ( 'NONE', ( #11301, #9801, #9941 ) ) ;
#7904=FACE_OUTER_BOUND ( 'NONE', #2324, .T. ) ;
#7907=DIRECTION ( 'NONE',  ( 1.000000000000000000, 0.000000000000000000, 0.000000000000000000 ) ) ;
#7919=CARTESIAN_POINT ( 'NONE',  ( 4.180704885107411783, 3.359771601077107039, -5.901655677627842600 ) ) ;
#7927=EDGE_CURVE ( 'NONE', #1664, #6455, #5609, .T. ) ;
#7928=DIRECTION ( 'NONE',  ( 0.000000000000000000, -0.000000000000000000, 1.000000000000000000 ) ) ;
#7933=VERTEX_POINT ( 'NONE', #4703 ) ;
#7952=VERTEX_POINT ( 'NONE', #3198 ) ;
#7954=CARTESIAN_POINT ( 'NONE',  ( 0.000000000000000000, 0.000000000000000000, -1.239675197676287643 ) ) ;
#7966=CONICAL_SURFACE ( 'NONE', #2791, 5.000000000000000888, 1.047197551196596299 ) ;
#7972=CARTESIAN_POINT ( 'NONE',  ( 0.000000000000000000, 0.000000000000000000, -2.617914285714285416 ) ) ;
#7980=DIRECTION ( 'NONE',  ( 1.000000000000000000, 0.000000000000000000, 0.000000000000000000 ) ) ;
#7981=EDGE_LOOP ( 'NONE', ( #6793, #4091, #11688, #4520, #11035, #8323 ) ) ;
#7984=CARTESIAN_POINT ( 'NONE',  ( 2.500000000000003109, -4.330127018922193649, -6.099999999999999645 ) ) ;
#7987=EDGE_LOOP ( 'NONE', ( #11194, #8734, #10621, #10763 ) ) ;
#7995=( NAMED_UNIT ( * ) PLANE_ANGLE_UNIT ( ) SI_UNIT ( $, .RADIAN. ) );
#8002=ORIENTED_EDGE ( 'NONE', *, *, #10682, .F. ) ;
#8011=DIRECTION ( 'NONE',  ( 0.000000000000000000, 0.000000000000000000, 1.000000000000000000 ) ) ;
#8018=DIRECTION ( 'NONE',  ( 1.000000000000000000, 0.000000000000000000, 0.000000000000000000 ) ) ;
#8019=( GEOMETRIC_REPRESENTATION_CONTEXT ( 3 ) GLOBAL_UNCERTAINTY_ASSIGNED_CONTEXT ( ( #8381 ) ) GLOBAL_UNIT_ASSIGNED_CONTEXT ( ( #3391, #1422, #3275 ) ) REPRESENTATION_CONTEXT ( 'NONE', 'WORKASPACE' ) );
#8020=FACE_OUTER_BOUND ( 'NONE', #9031, .T. ) ;
#8028=EDGE_LOOP ( 'NONE', ( #11027, #8152, #10297, #4069 ) ) ;
#8032=CARTESIAN_POINT ( 'NONE',  ( -2.500000000000000000, 3.061616997868383141E-16, -2.267810516609437776 ) ) ;
#8033=CARTESIAN_POINT ( 'NONE',  ( 0.000000000000000000, 0.000000000000000000, -6.099999999999999645 ) ) ;
#8036=CARTESIAN_POINT ( 'NONE',  ( 0.000000000000000000, 0.000000000000000000, 0.000000000000000000 ) ) ;
#8047=ORIENTED_EDGE ( 'NONE', *, *, #2613, .T. ) ;
#8057=CIRCLE ( 'NONE', #7874, 3.000000000000000000 ) ;
#8061=CARTESIAN_POINT ( 'NONE',  ( 2.925285743277525885, 4.084588180558403003, -0.01055556052338900083 ) ) ;
#8069=CIRCLE ( 'NONE', #9390, 5.000000000000000888 ) ;
#8074=EDGE_CURVE ( 'NONE', #1664, #8222, #1517, .T. ) ;
#8075=EDGE_CURVE ( 'NONE', #11030, #541, #5204, .T. ) ;
#8076=CARTESIAN_POINT ( 'NONE',  ( 0.000000000000000000, 0.000000000000000000, -6.074599999999999334 ) ) ;
#8078=AXIS2_PLACEMENT_3D ( 'NONE', #6986, #11629, #6325 ) ;
#8081=ADVANCED_FACE ( 'NONE', ( #4155 ), #7312, .T. ) ;
#8086=DIRECTION ( 'NONE',  ( -0.000000000000000000, 0.000000000000000000, -1.000000000000000000 ) ) ;
#8087=B_SPLINE_CURVE_WITH_KNOTS ( 'NONE', 3,
 ( #11316, #1386, #1439, #1499 ),
 .UNSPECIFIED., .F., .F.,
 ( 4, 4 ),
 ( 2.380735201026667963E-07, 0.002921158011986725936 ),
 .UNSPECIFIED. ) ;
#8088=ORIENTED_EDGE ( 'NONE', *, *, #8943, .F. ) ;
#8092=ORIENTED_EDGE ( 'NONE', *, *, #190, .F. ) ;
#8096=CARTESIAN_POINT ( 'NONE',  ( 0.000000000000000000, 0.000000000000000000, -5.560532340533429263 ) ) ;
#8120=ORIENTED_EDGE ( 'NONE', *, *, #602, .F. ) ;
#8134=CARTESIAN_POINT ( 'NONE',  ( -4.592054218142292754, -3.122278952918454920, -5.789399939901068493 ) ) ;
#8144=ADVANCED_FACE ( 'NONE', ( #5975 ), #11113, .F. ) ;
#8145=EDGE_LOOP ( 'NONE', ( #8916, #5724, #1587, #1040 ) ) ;
#8147=CARTESIAN_POINT ( 'NONE',  ( 0.000000000000000000, 0.000000000000000000, -6.099999999999999645 ) ) ;
#8151=CIRCLE ( 'NONE', #5101, 3.000000000000000000 ) ;
#8152=ORIENTED_EDGE ( 'NONE', *, *, #8074, .T. ) ;
#8176=VERTEX_POINT ( 'NONE', #9898 ) ;
#8181=ORIENTED_EDGE ( 'NONE', *, *, #1316, .F. ) ;
#8182=EDGE_CURVE ( 'NONE', #6801, #6451, #8259, .T. ) ;
#8188=AXIS2_PLACEMENT_3D ( 'NONE', #765, #651, #11784 ) ;
#8192=CARTESIAN_POINT ( 'NONE',  ( 5.000000000000000000, 2.886751345948134428, -5.653418012614792154 ) ) ;
#8195=CARTESIAN_POINT ( 'NONE',  ( -3.556264818047240706, -3.720292241887095397, -6.018341802876227220 ) ) ;
#8196=EDGE_CURVE ( 'NONE', #2740, #1955, #9605, .T. ) ;
#8203=ORIENTED_EDGE ( 'NONE', *, *, #2947, .T. ) ;
#8205=FACE_OUTER_BOUND ( 'NONE', #11078, .T. ) ;
#8209=ADVANCED_FACE ( 'NONE', ( #11071 ), #1694, .F. ) ;
#8221=AXIS2_PLACEMENT_3D ( 'NONE', #5099, #8401, #5943 ) ;
#8222=VERTEX_POINT ( 'NONE', #5416 ) ;
#8223=ADVANCED_FACE ( 'NONE', ( #9009 ), #2337, .F. ) ;
#8236=CIRCLE ( 'NONE', #5565, 2.500000000000000000 ) ;
#8253=ORIENTED_EDGE ( 'NONE', *, *, #6601, .F. ) ;
#8259=CIRCLE ( 'NONE', #4624, 3.000000000000000000 ) ;
#8260=DIRECTION ( 'NONE',  ( -0.000000000000000000, -0.000000000000000000, -1.000000000000000000 ) ) ;
#8263=DIRECTION ( 'NONE',  ( 0.000000000000000000, 0.000000000000000000, 1.000000000000000000 ) ) ;
#8276=CARTESIAN_POINT ( 'NONE',  ( 2.500000000000000000, 0.000000000000000000, -1.239675197676287643 ) ) ;
#8287=DIRECTION ( 'NONE',  ( -0.000000000000000000, -0.000000000000000000, -1.000000000000000000 ) ) ;
#8291=EDGE_LOOP ( 'NONE', ( #4526, #7348, #8527, #9609 ) ) ;
#8297=DIRECTION ( 'NONE',  ( -0.000000000000000000, -0.000000000000000000, -1.000000000000000000 ) ) ;
#8306=CARTESIAN_POINT ( 'NONE',  ( 5.000000000000000888, 0.000000000000000000, 0.000000000000000000 ) ) ;
#8318=DIRECTION ( 'NONE',  ( -1.000000000000000000, 0.000000000000000000, 0.000000000000000000 ) ) ;
#8319=CARTESIAN_POINT ( 'NONE',  ( 3.000000000000000000, 3.673940397442059868E-16, -4.346257142857142597 ) ) ;
#8323=ORIENTED_EDGE ( 'NONE', *, *, #9382, .F. ) ;
#8331=CARTESIAN_POINT ( 'NONE',  ( 0.000000000000000000, 0.000000000000000000, -0.02539999999999996774 ) ) ;
#8332=ORIENTED_EDGE ( 'NONE', *, *, #2436, .T. ) ;
#8351=CARTESIAN_POINT ( 'NONE',  ( 5.000000000000000000, 2.419979747126330683, -0.3118366332702858790 ) ) ;
#8355=EDGE_CURVE ( 'NONE', #6384, #10958, #789, .T. ) ;
#8356=AXIS2_PLACEMENT_3D ( 'NONE', #8033, #11733, #5278 ) ;
#8367=AXIS2_PLACEMENT_3D ( 'NONE', #6331, #5420, #10793 ) ;
#8377=FACE_BOUND ( 'NONE', #8840, .T. ) ;
#8381=UNCERTAINTY_MEASURE_WITH_UNIT (LENGTH_MEASURE( 1.000000000000000082E-05 ), #3391, 'distance_accuracy_value', 'NONE');
#8388=AXIS2_PLACEMENT_3D ( 'NONE', #9758, #8695, #534 ) ;
#8391=ORIENTED_EDGE ( 'NONE', *, *, #5286, .T. ) ;
#8401=DIRECTION ( 'NONE',  ( -0.000000000000000000, -0.000000000000000000, -1.000000000000000000 ) ) ;
#8407=EDGE_LOOP ( 'NONE', ( #6025, #6751, #10396, #6183 ) ) ;
#8409=CARTESIAN_POINT ( 'NONE',  ( 1.034159948410326981E-15, 5.773502691896260863, -6.099999999999999645 ) ) ;
#8411=ORIENTED_EDGE ( 'NONE', *, *, #5783, .T. ) ;
#8415=VECTOR ( 'NONE', #9089, 1000.000000000000000 ) ;
#8416=DIRECTION ( 'NONE',  ( 0.000000000000000000, 0.000000000000000000, 1.000000000000000000 ) ) ;
#8424=VERTEX_POINT ( 'NONE', #653 ) ;
#8430=CIRCLE ( 'NONE', #1150, 2.500000000000000000 ) ;
#8431=CARTESIAN_POINT ( 'NONE',  ( 0.000000000000000000, 0.000000000000000000, -0.3755037691048591086 ) ) ;
#8441=CIRCLE ( 'NONE', #3088, 3.000000000000000888 ) ;
#8445=CARTESIAN_POINT ( 'NONE',  ( 0.000000000000000000, 0.000000000000000000, -4.696360911962001339 ) ) ;
#8446=DIRECTION ( 'NONE',  ( 0.000000000000000000, -0.000000000000000000, 1.000000000000000000 ) ) ;
#8447=DIRECTION ( 'NONE',  ( -1.000000000000000000, 0.000000000000000000, 0.000000000000000000 ) ) ;
#8454=AXIS2_PLACEMENT_3D ( 'NONE', #9042, #3702, #11728 ) ;
#8455=AXIS2_PLACEMENT_3D ( 'NONE', #6266, #10851, #5299 ) ;
#8472=ORIENTED_EDGE ( 'NONE', *, *, #10909, .F. ) ;
#8479=CARTESIAN_POINT ( 'NONE',  ( 5.000000000000000000, 2.886751345948134428, -0.4465819873852071575 ) ) ;
#8514=EDGE_CURVE ( 'NONE', #3681, #8959, #5846, .T. ) ;
#8515=DIRECTION ( 'NONE',  ( -0.000000000000000000, -0.000000000000000000, -1.000000000000000000 ) ) ;
#8519=ORIENTED_EDGE ( 'NONE', *, *, #6101, .T. ) ;
#8527=ORIENTED_EDGE ( 'NONE', *, *, #4691, .T. ) ;
#8530=VERTEX_POINT ( 'NONE', #3182 ) ;
#8531=EDGE_CURVE ( 'NONE', #5005, #3681, #11254, .T. ) ;
#8535=CARTESIAN_POINT ( 'NONE',  ( -2.500000000000000000, 3.061616997868383141E-16, -2.968018054819144158 ) ) ;
#8543=AXIS2_PLACEMENT_3D ( 'NONE', #1348, #1406, #7587 ) ;
#8549=EDGE_CURVE ( 'NONE', #7933, #1507, #6221, .T. ) ;
#8558=DIRECTION ( 'NONE',  ( -0.000000000000000000, -0.000000000000000000, -1.000000000000000000 ) ) ;
#8560=CIRCLE ( 'NONE', #3385, 2.500000000000000000 ) ;
#8561=VERTEX_POINT ( 'NONE', #7358 ) ;
#8566=DIRECTION ( 'NONE',  ( -0.000000000000000000, -0.000000000000000000, -1.000000000000000000 ) ) ;
#8567=LINE ( 'NONE', #4013, #9928 ) ;
#8581=CIRCLE ( 'NONE', #9714, 3.000000000000000000 ) ;
#8584=EDGE_CURVE ( 'NONE', #9858, #11030, #8928, .T. ) ;
#8597=DIRECTION ( 'NONE',  ( -0.8191520442889885789, 1.003171929053520802E-16, 0.5735764363510507113 ) ) ;
#8605=DIRECTION ( 'NONE',  ( 0.000000000000000000, 0.000000000000000000, -1.000000000000000000 ) ) ;
#8608=CARTESIAN_POINT ( 'NONE',  ( 0.000000000000000000, 5.773502691896260863, -0.4465819873852071575 ) ) ;
#8620=CARTESIAN_POINT ( 'NONE',  ( -5.000000000000000000, -2.886751345948134428, -0.4465819873852071575 ) ) ;
#8622=ORIENTED_EDGE ( 'NONE', *, *, #5148, .T. ) ;
#8627=EDGE_CURVE ( 'NONE', #5840, #10958, #2049, .T. ) ;
#8633=ORIENTED_EDGE ( 'NONE', *, *, #741, .T. ) ;
#8638=AXIS2_PLACEMENT_3D ( 'NONE', #5758, #11359, #3113 ) ;
#8640=ORIENTED_EDGE ( 'NONE', *, *, #11241, .T. ) ;
#8641=AXIS2_PLACEMENT_3D ( 'NONE', #3583, #2802, #6353 ) ;
#8642=AXIS2_PLACEMENT_3D ( 'NONE', #6553, #8515, #10417 ) ;
#8646=ORIENTED_EDGE ( 'NONE', *, *, #6101, .F. ) ;
#8649=CARTESIAN_POINT ( 'NONE',  ( 3.000000000000000000, 3.673940397442059868E-16, -4.346257142857142597 ) ) ;
#8673=VERTEX_POINT ( 'NONE', #6683 ) ;
#8693=AXIS2_PLACEMENT_3D ( 'NONE', #11657, #10698, #5266 ) ;
#8695=DIRECTION ( 'NONE',  ( -0.000000000000000000, -0.000000000000000000, -1.000000000000000000 ) ) ;
#8704=CARTESIAN_POINT ( 'NONE',  ( 0.000000000000000000, 0.000000000000000000, -6.099999999999997868 ) ) ;
#8706=LINE ( 'NONE', #8649, #7406 ) ;
#8709=DIRECTION ( 'NONE',  ( -0.000000000000000000, -0.000000000000000000, -1.000000000000000000 ) ) ;
#8715=LINE ( 'NONE', #2301, #5481 ) ;
#8719=ORIENTED_EDGE ( 'NONE', *, *, #7570, .T. ) ;
#8731=CONICAL_SURFACE ( 'NONE', #6445, 5.000000000000000888, 1.047197551196596299 ) ;
#8734=ORIENTED_EDGE ( 'NONE', *, *, #1684, .T. ) ;
#8739=CARTESIAN_POINT ( 'NONE',  ( -5.000000000000000000, 2.886751345948126879, -6.099999999999999645 ) ) ;
#8743=VERTEX_POINT ( 'NONE', #1147 ) ;
#8745=CARTESIAN_POINT ( 'NONE',  ( -3.000000000000000888, 3.673940397442060854E-16, -25.03750572909317285 ) ) ;
#8754=DIRECTION ( 'NONE',  ( -1.000000000000000000, 0.000000000000000000, 0.000000000000000000 ) ) ;
#8786=ORIENTED_EDGE ( 'NONE', *, *, #931, .T. ) ;
#8789=B_SPLINE_CURVE_WITH_KNOTS ( 'NONE', 3,
 ( #7708, #10388, #2243, #608, #4054, #11340, #7039, #8608 ),
 .UNSPECIFIED., .F., .F.,
 ( 4, 2, 2, 4 ),
 ( 0.002921158011986710757, 0.003648658599403065313, 0.004376159186819420302, 0.005831160361652131148 ),
 .UNSPECIFIED. ) ;
#8792=EDGE_CURVE ( 'NONE', #1955, #8561, #1766, .T. ) ;
#8799=CARTESIAN_POINT ( 'NONE',  ( 0.000000000000000000, 0.000000000000000000, -3.131981945180866589 ) ) ;
#8800=DIRECTION ( 'NONE',  ( -0.000000000000000000, -0.000000000000000000, -1.000000000000000000 ) ) ;
#8805=EDGE_CURVE ( 'NONE', #9206, #9472, #7871, .T. ) ;
#8816=CARTESIAN_POINT ( 'NONE',  ( 2.925285743277525441, 4.084588180558403003, -6.089444439476610071 ) ) ;
#8819=ORIENTED_EDGE ( 'NONE', *, *, #5073, .F. ) ;
#8825=CIRCLE ( 'NONE', #10720, 3.000000000000000000 ) ;
#8835=CARTESIAN_POINT ( 'NONE',  ( 3.000000000000000000, 3.673940397442059868E-16, -3.482085714285714229 ) ) ;
#8839=DIRECTION ( 'NONE',  ( 1.000000000000000000, 0.000000000000000000, 0.000000000000000000 ) ) ;
#8840=EDGE_LOOP ( 'NONE', ( #3944, #10904 ) ) ;
#8846=CONICAL_SURFACE ( 'NONE', #577, 5.000000000000000888, 1.047197551196596299 ) ;
#8854=FACE_OUTER_BOUND ( 'NONE', #8028, .T. ) ;
#8861=DIRECTION ( 'NONE',  ( -0.8191520442889974607, 0.000000000000000000, -0.5735764363510379438 ) ) ;
#8871=ADVANCED_FACE ( 'NONE', ( #6080 ), #609, .F. ) ;
#8882=FACE_BOUND ( 'NONE', #3531, .T. ) ;
#8885=CARTESIAN_POINT ( 'NONE',  ( 5.000000000000000000, 2.419979747126329350, -5.788163366729714099 ) ) ;
#8887=ADVANCED_FACE ( 'NONE', ( #6021 ), #2411, .F. ) ;
#8894=ORIENTED_EDGE ( 'NONE', *, *, #2655, .F. ) ;
#8916=ORIENTED_EDGE ( 'NONE', *, *, #5414, .F. ) ;
#8926=EDGE_CURVE ( 'NONE', #2315, #11218, #8706, .T. ) ;
#8928=B_SPLINE_CURVE_WITH_KNOTS ( 'NONE', 3,
 ( #926, #1887, #11045, #1173, #10089, #5742 ),
 .UNSPECIFIED., .F., .F.,
 ( 4, 2, 4 ),
 ( 0.005150343764683555127, 0.006610526168996384844, 0.008070708573309213693 ),
 .UNSPECIFIED. ) ;
#8943=EDGE_CURVE ( 'NONE', #8561, #2740, #11049, .T. ) ;
#8947=AXIS2_PLACEMENT_3D ( 'NONE', #9493, #323, #11154 ) ;
#8952=EDGE_CURVE ( 'NONE', #9962, #8176, #6375, .T. ) ;
#8955=DIRECTION ( 'NONE',  ( -0.000000000000000000, -0.000000000000000000, 1.000000000000000000 ) ) ;
#8959=VERTEX_POINT ( 'NONE', #10780 ) ;
#8969=EDGE_LOOP ( 'NONE', ( #1847, #4787, #10775 ) ) ;
#8984=VECTOR ( 'NONE', #10243, 1000.000000000000000 ) ;
#8985=VERTEX_POINT ( 'NONE', #2591 ) ;
#8987=AXIS2_PLACEMENT_3D ( 'NONE', #11662, #2627, #9809 ) ;
#8990=DIRECTION ( 'NONE',  ( -1.000000000000000000, 0.000000000000000000, 0.000000000000000000 ) ) ;
#8992=AXIS2_PLACEMENT_3D ( 'NONE', #993, #11107, #9322 ) ;
#8997=DIRECTION ( 'NONE',  ( 0.000000000000000000, 0.000000000000000000, 1.000000000000000000 ) ) ;
#8998=VERTEX_POINT ( 'NONE', #11800 ) ;
#9003=DIRECTION ( 'NONE',  ( 0.000000000000000000, 0.000000000000000000, 1.000000000000000000 ) ) ;
#9009=FACE_OUTER_BOUND ( 'NONE', #605, .T. ) ;
#9011=FACE_OUTER_BOUND ( 'NONE', #1053, .T. ) ;
#9012=AXIS2_PLACEMENT_3D ( 'NONE', #5730, #10260, #2118 ) ;
#9013=ORIENTED_EDGE ( 'NONE', *, *, #4777, .F. ) ;
#9014=AXIS2_PLACEMENT_3D ( 'NONE', #7690, #11324, #5898 ) ;
#9016=EDGE_CURVE ( 'NONE', #8530, #9830, #6798, .T. ) ;
#9021=AXIS2_PLACEMENT_3D ( 'NONE', #1098, #9365, #379 ) ;
#9029=CARTESIAN_POINT ( 'NONE',  ( 0.000000000000000000, 0.000000000000000000, -3.482085714285714229 ) ) ;
#9031=EDGE_LOOP ( 'NONE', ( #9710, #4468, #3977, #11578 ) ) ;
#9039=CARTESIAN_POINT ( 'NONE',  ( 0.000000000000000000, 0.000000000000000000, -0.5394676594665810399 ) ) ;
#9041=ORIENTED_EDGE ( 'NONE', *, *, #5370, .F. ) ;
#9042=CARTESIAN_POINT ( 'NONE',  ( 0.000000000000000000, 0.000000000000000000, -0.3755037691048591086 ) ) ;
#9045=EDGE_CURVE ( 'NONE', #306, #4164, #9887, .T. ) ;
#9047=DIRECTION ( 'NONE',  ( -0.000000000000000000, -0.000000000000000000, -1.000000000000000000 ) ) ;
#9060=DIRECTION ( 'NONE',  ( -1.000000000000000000, 0.000000000000000000, 0.000000000000000000 ) ) ;
#9064=DIRECTION ( 'NONE',  ( -1.000000000000000000, 0.000000000000000000, 0.000000000000000000 ) ) ;
#9087=CARTESIAN_POINT ( 'NONE',  ( 4.999999999999999112, -0.4878135028931883110, -6.100000000000002309 ) ) ;
#9089=DIRECTION ( 'NONE',  ( 0.8191520442889885789, 0.000000000000000000, 0.5735764363510507113 ) ) ;
#9107=VERTEX_POINT ( 'NONE', #719 ) ;
#9112=CARTESIAN_POINT ( 'NONE',  ( -2.500000000000000000, 3.061616997868383141E-16, -4.696360911962001339 ) ) ;
#9114=ORIENTED_EDGE ( 'NONE', *, *, #3450, .F. ) ;
#9125=CARTESIAN_POINT ( 'NONE',  ( 2.712167343862819546, 4.207632145829744985, 4.204248033696719733E-15 ) ) ;
#9141=ORIENTED_EDGE ( 'NONE', *, *, #9821, .F. ) ;
#9149=DIRECTION ( 'NONE',  ( -1.000000000000000000, 0.000000000000000000, 0.000000000000000000 ) ) ;
#9155=ORIENTED_EDGE ( 'NONE', *, *, #2646, .F. ) ;
#9185=ORIENTED_EDGE ( 'NONE', *, *, #1627, .T. ) ;
#9194=AXIS2_PLACEMENT_3D ( 'NONE', #9395, #9456, #6719 ) ;
#9197=ORIENTED_EDGE ( 'NONE', *, *, #8196, .F. ) ;
#9199=AXIS2_PLACEMENT_3D ( 'NONE', #5111, #1566, #10597 ) ;
#9203=DIRECTION ( 'NONE',  ( -1.000000000000000000, 0.000000000000000000, 0.000000000000000000 ) ) ;
#9206=VERTEX_POINT ( 'NONE', #5645 ) ;
#9210=PLANE ( 'NONE',  #1378 ) ;
#9213=CARTESIAN_POINT ( 'NONE',  ( 0.000000000000000000, 0.000000000000000000, -6.099999999999999645 ) ) ;
#9222=ORIENTED_EDGE ( 'NONE', *, *, #2572, .F. ) ;
#9227=ADVANCED_FACE ( 'NONE', ( #3962 ), #2821, .F. ) ;
#9228=DIRECTION ( 'NONE',  ( -1.000000000000000000, 0.000000000000000000, 0.000000000000000000 ) ) ;
#9229=DIRECTION ( 'NONE',  ( 1.000000000000000000, 0.000000000000000000, 0.000000000000000000 ) ) ;
#9235=DIRECTION ( 'NONE',  ( 1.000000000000000000, 0.000000000000000000, 0.000000000000000000 ) ) ;
#9242=VERTEX_POINT ( 'NONE', #6067 ) ;
#9243=DIRECTION ( 'NONE',  ( 0.000000000000000000, 0.000000000000000000, 1.000000000000000000 ) ) ;
#9248=CARTESIAN_POINT ( 'NONE',  ( 2.500000000000000000, 0.000000000000000000, -6.099999999999999645 ) ) ;
#9268=ORIENTED_EDGE ( 'NONE', *, *, #4299, .T. ) ;
#9270=DIRECTION ( 'NONE',  ( -1.000000000000000000, 0.000000000000000000, 0.000000000000000000 ) ) ;
#9272=CARTESIAN_POINT ( 'NONE',  ( -2.500000000000000000, 3.061616997868383141E-16, -3.832189483390572970 ) ) ;
#9275=CIRCLE ( 'NONE', #1247, 3.000000000000000000 ) ;
#9285=VECTOR ( 'NONE', #2141, 1000.000000000000000 ) ;
#9289=LINE ( 'NONE', #8745, #7461 ) ;
#9293=CIRCLE ( 'NONE', #5107, 2.500000000000000000 ) ;
#9300=EDGE_LOOP ( 'NONE', ( #807, #2466, #7771, #4189 ) ) ;
#9303=ADVANCED_FACE ( 'NONE', ( #7680 ), #10449, .F. ) ;
#9310=VECTOR ( 'NONE', #3052, 1000.000000000000114 ) ;
#9312=VERTEX_POINT ( 'NONE', #4022 ) ;
#9322=DIRECTION ( 'NONE',  ( -1.000000000000000000, 0.000000000000000000, 0.000000000000000000 ) ) ;
#9324=ORIENTED_EDGE ( 'NONE', *, *, #1191, .T. ) ;
#9329=DIRECTION ( 'NONE',  ( 0.000000000000000000, 0.000000000000000000, -1.000000000000000000 ) ) ;
#9335=DIRECTION ( 'NONE',  ( -0.000000000000000000, -0.000000000000000000, 1.000000000000000000 ) ) ;
#9339=AXIS2_PLACEMENT_3D ( 'NONE', #7972, #3532, #1732 ) ;
#9340=ORIENTED_EDGE ( 'NONE', *, *, #4904, .F. ) ;
#9345=DIRECTION ( 'NONE',  ( 1.000000000000000000, 0.000000000000000000, 0.000000000000000000 ) ) ;
#9352=AXIS2_PLACEMENT_3D ( 'NONE', #6105, #2438, #3217 ) ;
#9356=CARTESIAN_POINT ( 'NONE',  ( -2.500000000000000000, 3.061616997868383141E-16, -0.5394676594665810399 ) ) ;
#9361=DIRECTION ( 'NONE',  ( -0.8191520442889974607, 0.000000000000000000, -0.5735764363510379438 ) ) ;
#9365=DIRECTION ( 'NONE',  ( 0.000000000000000000, 0.000000000000000000, 1.000000000000000000 ) ) ;
#9373=VECTOR ( 'NONE', #3767, 1000.000000000000000 ) ;
#9382=EDGE_CURVE ( 'NONE', #9830, #364, #8087, .T. ) ;
#9390=AXIS2_PLACEMENT_3D ( 'NONE', #429, #5966, #3911 ) ;
#9391=FACE_OUTER_BOUND ( 'NONE', #7742, .T. ) ;
#9395=CARTESIAN_POINT ( 'NONE',  ( 0.000000000000000000, 0.000000000000000000, -5.210428571428570521 ) ) ;
#9396=DIRECTION ( 'NONE',  ( -0.000000000000000000, -0.000000000000000000, 1.000000000000000000 ) ) ;
#9406=DIRECTION ( 'NONE',  ( -1.000000000000000000, 0.000000000000000000, 0.000000000000000000 ) ) ;
#9409=DIRECTION ( 'NONE',  ( -1.000000000000000000, 0.000000000000000000, 0.000000000000000000 ) ) ;
#9412=DIRECTION ( 'NONE',  ( -0.8191520442889913545, 0.000000000000000000, -0.5735764363510468256 ) ) ;
#9415=EDGE_LOOP ( 'NONE', ( #11089, #2778, #2422, #9013 ) ) ;
#9432=CARTESIAN_POINT ( 'NONE',  ( 0.000000000000000000, 0.000000000000000000, -3.832189483390572970 ) ) ;
#9454=SHAPE_REPRESENTATION ( 'hex nut gradec_iso_ISO - 4034 - M6 - S', ( #4738 ), #10420 ) ;
#9456=DIRECTION ( 'NONE',  ( -0.000000000000000000, -0.000000000000000000, -1.000000000000000000 ) ) ;
#9458=DIRECTION ( 'NONE',  ( -0.000000000000000000, -0.000000000000000000, -1.000000000000000000 ) ) ;
#9468=DIRECTION ( 'NONE',  ( -0.000000000000000000, -0.000000000000000000, -1.000000000000000000 ) ) ;
#9470=CARTESIAN_POINT ( 'NONE',  ( 5.000000000000000000, 2.886751345948124214, -6.099999999999999645 ) ) ;
#9472=VERTEX_POINT ( 'NONE', #4378 ) ;
#9478=AXIS2_PLACEMENT_3D ( 'NONE', #7418, #2796, #6462 ) ;
#9493=CARTESIAN_POINT ( 'NONE',  ( 1.034159948410326981E-15, 5.773502691896260863, -6.099999999999999645 ) ) ;
#9530=ADVANCED_FACE ( 'NONE', ( #4785 ), #10641, .F. ) ;
#9532=AXIS2_PLACEMENT_3D ( 'NONE', #8096, #10044, #8990 ) ;
#9541=DIRECTION ( 'NONE',  ( 1.000000000000000000, 0.000000000000000000, 0.000000000000000000 ) ) ;
#9542=DIRECTION ( 'NONE',  ( 0.000000000000000000, 0.000000000000000000, 1.000000000000000000 ) ) ;
#9546=AXIS2_PLACEMENT_3D ( 'NONE', #8076, #7353, #10026 ) ;
#9547=ORIENTED_EDGE ( 'NONE', *, *, #3572, .F. ) ;
#9554=CYLINDRICAL_SURFACE ( 'NONE', #8543, 2.500000000000000000 ) ;
#9561=AXIS2_PLACEMENT_3D ( 'NONE', #2798, #5622, #87 ) ;
#9565=AXIS2_PLACEMENT_3D ( 'NONE', #813, #8086, #7307 ) ;
#9567=ORIENTED_EDGE ( 'NONE', *, *, #2655, .T. ) ;
#9575=ADVANCED_FACE ( 'NONE', ( #8377, #157 ), #6410, .F. ) ;
#9577=CARTESIAN_POINT ( 'NONE',  ( 0.000000000000000000, 0.000000000000000000, -25.03750572909317285 ) ) ;
#9596=CARTESIAN_POINT ( 'NONE',  ( -2.500000000000000000, 3.061616997868383141E-16, -1.403639088038009630 ) ) ;
#9603=CIRCLE ( 'NONE', #9820, 2.500000000000000000 ) ;
#9605=CIRCLE ( 'NONE', #599, 5.000000000000000888 ) ;
#9609=ORIENTED_EDGE ( 'NONE', *, *, #6744, .T. ) ;
#9611=DIRECTION ( 'NONE',  ( 1.000000000000000000, 0.000000000000000000, 0.000000000000000000 ) ) ;
#9613=DIRECTION ( 'NONE',  ( 0.8191520442889885789, 0.000000000000000000, 0.5735764363510507113 ) ) ;
#9628=DIRECTION ( 'NONE',  ( -1.000000000000000000, 0.000000000000000000, 0.000000000000000000 ) ) ;
#9630=ORIENTED_EDGE ( 'NONE', *, *, #7835, .T. ) ;
#9637=EDGE_LOOP ( 'NONE', ( #4693, #11626, #7558, #7229 ) ) ;
#9640=ORIENTED_EDGE ( 'NONE', *, *, #2510, .F. ) ;
#9643=AXIS2_PLACEMENT_3D ( 'NONE', #9577, #9396, #4855 ) ;
#9648=CARTESIAN_POINT ( 'NONE',  ( 3.556264818047235821, 3.720292241887088736, -6.018341802876231661 ) ) ;
#9650=CARTESIAN_POINT ( 'NONE',  ( 2.500000000000003109, -4.330127018922193649, 0.000000000000000000 ) ) ;
#9653=ADVANCED_FACE ( 'NONE', ( #9391 ), #4928, .F. ) ;
#9655=DIRECTION ( 'NONE',  ( -1.000000000000000000, 0.000000000000000000, 0.000000000000000000 ) ) ;
#9690=CARTESIAN_POINT ( 'NONE',  ( -2.500000000000000000, 3.061616997868383141E-16, -0.3755037691048591086 ) ) ;
#9693=DIRECTION ( 'NONE',  ( 1.000000000000000000, 0.000000000000000000, 0.000000000000000000 ) ) ;
#9697=CYLINDRICAL_SURFACE ( 'NONE', #8987, 3.000000000000000888 ) ;
#9705=AXIS2_PLACEMENT_3D ( 'NONE', #9029, #8287, #7127 ) ;
#9708=ORIENTED_EDGE ( 'NONE', *, *, #8792, .F. ) ;
#9709=CARTESIAN_POINT ( 'NONE',  ( -2.500000000000000000, 3.061616997868383141E-16, -0.3755037691048591086 ) ) ;
#9710=ORIENTED_EDGE ( 'NONE', *, *, #3131, .F. ) ;
#9713=DIRECTION ( 'NONE',  ( 0.8191520442889974607, 1.003171929053531649E-16, -0.5735764363510379438 ) ) ;
#9714=AXIS2_PLACEMENT_3D ( 'NONE', #8331, #3065, #9409 ) ;
#9719=DIRECTION ( 'NONE',  ( -0.000000000000000000, -0.000000000000000000, -1.000000000000000000 ) ) ;
#9722=FILL_AREA_STYLE ('',( #1520 ) ) ;
#9758=CARTESIAN_POINT ( 'NONE',  ( 0.000000000000000000, 0.000000000000000000, -0.02539999999999996774 ) ) ;
#9763=CARTESIAN_POINT ( 'NONE',  ( 4.999999999999998224, -2.886751345948137981, -0.4465819873852071575 ) ) ;
#9775=CONICAL_SURFACE ( 'NONE', #9199, 3.000000000000000000, 0.9599310885968912466 ) ;
#9777=CARTESIAN_POINT ( 'NONE',  ( 4.999999999999999112, 0.4881033300985028744, -6.099999999999999645 ) ) ;
#9782=AXIS2_PLACEMENT_3D ( 'NONE', #9213, #3527, #5334 ) ;
#9783=SURFACE_STYLE_USAGE ( .BOTH. , #11572 ) ;
#9786=EDGE_CURVE ( 'NONE', #9107, #8222, #2048, .T. ) ;
#9801=ORIENTED_EDGE ( 'NONE', *, *, #8196, .T. ) ;
#9807=ORIENTED_EDGE ( 'NONE', *, *, #11024, .T. ) ;
#9809=DIRECTION ( 'NONE',  ( 1.000000000000000000, 0.000000000000000000, 0.000000000000000000 ) ) ;
#9817=DIRECTION ( 'NONE',  ( 1.000000000000000000, 0.000000000000000000, 0.000000000000000000 ) ) ;
#9820=AXIS2_PLACEMENT_3D ( 'NONE', #7546, #10283, #11167 ) ;
#9821=EDGE_CURVE ( 'NONE', #7952, #5798, #4968, .T. ) ;
#9830=VERTEX_POINT ( 'NONE', #6715 ) ;
#9839=CARTESIAN_POINT ( 'NONE',  ( -5.000000000000000888, 0.000000000000000000, 0.000000000000000000 ) ) ;
#9854=EDGE_LOOP ( 'NONE', ( #4126, #8181, #9324, #74 ) ) ;
#9855=CARTESIAN_POINT ( 'NONE',  ( 0.000000000000000000, 5.773502691896260863, -5.653418012614792154 ) ) ;
#9858=VERTEX_POINT ( 'NONE', #8620 ) ;
#9862=LINE ( 'NONE', #10755, #6120 ) ;
#9863=DIRECTION ( 'NONE',  ( -1.000000000000000000, 0.000000000000000000, 0.000000000000000000 ) ) ;
#9878=EDGE_LOOP ( 'NONE', ( #11543, #11453, #6958 ) ) ;
#9880=FACE_OUTER_BOUND ( 'NONE', #7987, .T. ) ;
#9883=AXIS2_PLACEMENT_3D ( 'NONE', #4731, #9458, #3768 ) ;
#9887=LINE ( 'NONE', #9112, #7031 ) ;
#9892=EDGE_LOOP ( 'NONE', ( #10751, #1638, #396, #11553 ) ) ;
#9893=CARTESIAN_POINT ( 'NONE',  ( 0.8179331680532999638, 5.301268757141563093, -0.1739375980333749683 ) ) ;
#9898=CARTESIAN_POINT ( 'NONE',  ( 3.000000000000000000, 3.673940397442059868E-16, -0.02539999999999996774 ) ) ;
#9913=ADVANCED_FACE ( 'NONE', ( #8854 ), #5890, .F. ) ;
#9928=VECTOR ( 'NONE', #409, 1000.000000000000000 ) ;
#9932=EDGE_CURVE ( 'NONE', #10233, #2213, #4548, .T. ) ;
#9934=ORIENTED_EDGE ( 'NONE', *, *, #3572, .T. ) ;
#9936=CYLINDRICAL_SURFACE ( 'NONE', #8356, 2.500000000000000000 ) ;
#9937=EDGE_CURVE ( 'NONE', #11519, #8176, #2440, .T. ) ;
#9940=AXIS2_PLACEMENT_3D ( 'NONE', #6739, #5715, #4991 ) ;
#9941=ORIENTED_EDGE ( 'NONE', *, *, #8792, .T. ) ;
#9954=CARTESIAN_POINT ( 'NONE',  ( -4.999999999999999112, 0.4881033300985023748, 4.497744949920333814E-16 ) ) ;
#9962=VERTEX_POINT ( 'NONE', #5318 ) ;
#9986=B_SPLINE_CURVE_WITH_KNOTS ( 'NONE', 3,
 ( #11213, #1217, #1157, #4884, #8351, #8479 ),
 .UNSPECIFIED., .F., .F.,
 ( 4, 2, 4 ),
 ( 0.008070708573309217163, 0.009531758523483289253, 0.01099280847365736134 ),
 .UNSPECIFIED. ) ;
#10003=CARTESIAN_POINT ( 'NONE',  ( 3.351853367131007122, -3.838309248099025961, -6.099999999999998757 ) ) ;
#10007=EDGE_CURVE ( 'NONE', #3733, #1955, #3205, .T. ) ;
#10014=CARTESIAN_POINT ( 'NONE',  ( 4.180704885107411783, 3.359771601077107483, -0.1983443223721572113 ) ) ;
#10020=ORIENTED_EDGE ( 'NONE', *, *, #10909, .T. ) ;
#10024=ORIENTED_EDGE ( 'NONE', *, *, #5414, .T. ) ;
#10025=ADVANCED_FACE ( 'NONE', ( #2111 ), #2239, .F. ) ;
#10026=DIRECTION ( 'NONE',  ( 1.000000000000000000, 0.000000000000000000, 0.000000000000000000 ) ) ;
#10029=ORIENTED_EDGE ( 'NONE', *, *, #439, .T. ) ;
#10037=ORIENTED_EDGE ( 'NONE', *, *, #4441, .T. ) ;
#10042=DIRECTION ( 'NONE',  ( -1.000000000000000000, 0.000000000000000000, 0.000000000000000000 ) ) ;
#10043=ORIENTED_EDGE ( 'NONE', *, *, #6551, .T. ) ;
#10044=DIRECTION ( 'NONE',  ( -0.000000000000000000, -0.000000000000000000, -1.000000000000000000 ) ) ;
#10052=ORIENTED_EDGE ( 'NONE', *, *, #2024, .F. ) ;
#10085=CONICAL_SURFACE ( 'NONE', #7439, 2.500000000000000000, 0.9599310885968755924 ) ;
#10089=CARTESIAN_POINT ( 'NONE',  ( -4.999999999999999112, -0.4878135028931870898, 5.217722955086490089E-16 ) ) ;
#10125=PRODUCT_CONTEXT ( 'NONE', #1863, 'mechanical' ) ;
#10143=DIRECTION ( 'NONE',  ( -1.000000000000000000, 0.000000000000000000, 0.000000000000000000 ) ) ;
#10145=CARTESIAN_POINT ( 'NONE',  ( 2.500000000000000000, 0.000000000000000000, -1.239675197676287643 ) ) ;
#10152=CARTESIAN_POINT ( 'NONE',  ( 4.999999999999999112, -2.417244626924489825, -0.3110470720778663600 ) ) ;
#10157=EDGE_CURVE ( 'NONE', #7832, #6451, #1271, .T. ) ;
#10158=ORIENTED_EDGE ( 'NONE', *, *, #11168, .F. ) ;
#10161=FACE_OUTER_BOUND ( 'NONE', #5501, .T. ) ;
#10186=FACE_OUTER_BOUND ( 'NONE', #11507, .T. ) ;
#10189=CARTESIAN_POINT ( 'NONE',  ( 2.500000000000000000, 0.000000000000000000, -6.099999999999999645 ) ) ;
#10195=CARTESIAN_POINT ( 'NONE',  ( -5.000000000000000000, 2.886751345948134428, -5.653418012614792154 ) ) ;
#10208=DIRECTION ( 'NONE',  ( -0.000000000000000000, -0.000000000000000000, -1.000000000000000000 ) ) ;
#10211=ORIENTED_EDGE ( 'NONE', *, *, #8355, .T. ) ;
#10219=EDGE_CURVE ( 'NONE', #9312, #8530, #4782, .T. ) ;
#10229=DIRECTION ( 'NONE',  ( 1.000000000000000000, 0.000000000000000000, 0.000000000000000000 ) ) ;
#10233=VERTEX_POINT ( 'NONE', #8276 ) ;
#10235=ORIENTED_EDGE ( 'NONE', *, *, #5148, .F. ) ;
#10240=LINE ( 'NONE', #240, #903 ) ;
#10243=DIRECTION ( 'NONE',  ( 0.000000000000000000, 0.000000000000000000, 1.000000000000000000 ) ) ;
#10245=CYLINDRICAL_SURFACE ( 'NONE', #11290, 2.500000000000000000 ) ;
#10260=DIRECTION ( 'NONE',  ( -0.000000000000000000, -0.000000000000000000, -1.000000000000000000 ) ) ;
#10262=AXIS2_PLACEMENT_3D ( 'NONE', #5951, #6851, #5159 ) ;
#10264=AXIS2_PLACEMENT_3D ( 'NONE', #8445, #8263, #3765 ) ;
#10268=LINE ( 'NONE', #10145, #556 ) ;
#10270=ORIENTED_EDGE ( 'NONE', *, *, #6770, .T. ) ;
#10278=VERTEX_POINT ( 'NONE', #1745 ) ;
#10283=DIRECTION ( 'NONE',  ( -0.000000000000000000, -0.000000000000000000, -1.000000000000000000 ) ) ;
#10297=ORIENTED_EDGE ( 'NONE', *, *, #5370, .T. ) ;
#10309=EDGE_CURVE ( 'NONE', #2213, #66, #7100, .T. ) ;
#10312=CONICAL_SURFACE ( 'NONE', #5162, 5.000000000000000888, 1.047197551196596299 ) ;
#10332=ORIENTED_EDGE ( 'NONE', *, *, #2646, .T. ) ;
#10343=CONICAL_SURFACE ( 'NONE', #2, 3.000000000000000000, 0.9599310885968912466 ) ;
#10356=EDGE_LOOP ( 'NONE', ( #8472, #7377, #10706, #4050 ) ) ;
#10363=FACE_OUTER_BOUND ( 'NONE', #6286, .T. ) ;
#10366=DIRECTION ( 'NONE',  ( 0.000000000000000000, -0.000000000000000000, 1.000000000000000000 ) ) ;
#10374=DIRECTION ( 'NONE',  ( 0.000000000000000000, 0.000000000000000000, 1.000000000000000000 ) ) ;
#10382=ADVANCED_FACE ( 'NONE', ( #10781 ), #10085, .F. ) ;
#10383=DIRECTION ( 'NONE',  ( 1.000000000000000000, 0.000000000000000000, 0.000000000000000000 ) ) ;
#10385=FACE_OUTER_BOUND ( 'NONE', #11795, .T. ) ;
#10388=CARTESIAN_POINT ( 'NONE',  ( -2.287832656137187115, 4.452621892014636096, 3.582384678254184149E-15 ) ) ;
#10390=EDGE_LOOP ( 'NONE', ( #854, #858, #7608, #3020, #2252, #3711 ) ) ;
#10395=CARTESIAN_POINT ( 'NONE',  ( -3.000000000000000000, 0.000000000000000000, -1.753742857142857048 ) ) ;
#10396=ORIENTED_EDGE ( 'NONE', *, *, #5219, .T. ) ;
#10406=EDGE_CURVE ( 'NONE', #52, #6251, #11424, .T. ) ;
#10407=CARTESIAN_POINT ( 'NONE',  ( 0.000000000000000000, 0.000000000000000000, -6.099999999999999645 ) ) ;
#10417=DIRECTION ( 'NONE',  ( -1.000000000000000000, 0.000000000000000000, 0.000000000000000000 ) ) ;
#10420=( GEOMETRIC_REPRESENTATION_CONTEXT ( 3 ) GLOBAL_UNCERTAINTY_ASSIGNED_CONTEXT ( ( #6768 ) ) GLOBAL_UNIT_ASSIGNED_CONTEXT ( ( #11276, #7995, #7818 ) ) REPRESENTATION_CONTEXT ( 'NONE', 'WORKASPACE' ) );
#10428=DIRECTION ( 'NONE',  ( 0.000000000000000000, 0.000000000000000000, 1.000000000000000000 ) ) ;
#10435=DIRECTION ( 'NONE',  ( 0.8191520442889974607, 1.003171929053531649E-16, -0.5735764363510379438 ) ) ;
#10438=CARTESIAN_POINT ( 'NONE',  ( 2.500000000000000000, 0.000000000000000000, -5.560532340533429263 ) ) ;
#10449=CONICAL_SURFACE ( 'NONE', #10262, 3.000000000000000000, 0.9599310885968912466 ) ;
#10473=ADVANCED_FACE ( 'NONE', ( #1077 ), #4744, .T. ) ;
#10482=EDGE_CURVE ( 'NONE', #8176, #9472, #8581, .T. ) ;
#10483=DIRECTION ( 'NONE',  ( -0.000000000000000000, -0.000000000000000000, -1.000000000000000000 ) ) ;
#10491=AXIS2_PLACEMENT_3D ( 'NONE', #632, #4294, #7066 ) ;
#10492=ORIENTED_EDGE ( 'NONE', *, *, #4994, .F. ) ;
#10503=ORIENTED_EDGE ( 'NONE', *, *, #5219, .F. ) ;
#10505=VECTOR ( 'NONE', #5498, 999.9999999999998863 ) ;
#10511=ORIENTED_EDGE ( 'NONE', *, *, #9786, .F. ) ;
#10519=DIRECTION ( 'NONE',  ( -0.8191520442889885789, 1.003171929053520802E-16, 0.5735764363510507113 ) ) ;
#10521=ADVANCED_FACE ( 'NONE', ( #7384 ), #6674, .F. ) ;
#10530=PRODUCT ( 'hex nut gradec_iso_ISO - 4034 - M6 - S', 'hex nut gradec_iso_ISO - 4034 - M6 - S', '', ( #10125 ) ) ;
#10536=DIRECTION ( 'NONE',  ( -0.000000000000000000, -0.000000000000000000, 1.000000000000000000 ) ) ;
#10538=ORIENTED_EDGE ( 'NONE', *, *, #10007, .T. ) ;
#10540=ADVANCED_FACE ( 'NONE', ( #10186 ), #7568, .F. ) ;
#10548=EDGE_CURVE ( 'NONE', #5996, #2213, #10240, .T. ) ;
#10555=CARTESIAN_POINT ( 'NONE',  ( -2.287832656137187115, 4.452621892014636984, -6.100000000000003197 ) ) ;
#10576=ORIENTED_EDGE ( 'NONE', *, *, #3567, .T. ) ;
#10584=ORIENTED_EDGE ( 'NONE', *, *, #1838, .F. ) ;
#10586=DIRECTION ( 'NONE',  ( -0.000000000000000000, -0.000000000000000000, -1.000000000000000000 ) ) ;
#10591=DIRECTION ( 'NONE',  ( 1.000000000000000000, 0.000000000000000000, 0.000000000000000000 ) ) ;
#10597=DIRECTION ( 'NONE',  ( -1.000000000000000000, 0.000000000000000000, 0.000000000000000000 ) ) ;
#10612=EDGE_LOOP ( 'NONE', ( #4275, #11495, #8646 ) ) ;
#10620=AXIS2_PLACEMENT_3D ( 'NONE', #8799, #578, #520 ) ;
#10621=ORIENTED_EDGE ( 'NONE', *, *, #2947, .F. ) ;
#10624=AXIS2_PLACEMENT_3D ( 'NONE', #2230, #9542, #4272 ) ;
#10628=ORIENTED_EDGE ( 'NONE', *, *, #8531, .F. ) ;
#10632=DIRECTION ( 'NONE',  ( -1.000000000000000000, 0.000000000000000000, 0.000000000000000000 ) ) ;
#10634=DIRECTION ( 'NONE',  ( -0.000000000000000000, -0.000000000000000000, 1.000000000000000000 ) ) ;
#10641=CONICAL_SURFACE ( 'NONE', #6651, 3.000000000000000888, 0.9599310885968804774 ) ;
#10663=CIRCLE ( 'NONE', #9532, 2.500000000000000000 ) ;
#10668=EDGE_CURVE ( 'NONE', #9472, #8176, #338, .T. ) ;
#10669=CARTESIAN_POINT ( 'NONE',  ( -5.000000000000000000, 1.947085426416875764, -0.1996207071196899330 ) ) ;
#10682=EDGE_CURVE ( 'NONE', #8673, #3954, #6125, .T. ) ;
#10689=EDGE_CURVE ( 'NONE', #1507, #10278, #4946, .T. ) ;
#10698=DIRECTION ( 'NONE',  ( -1.000000000000000000, 0.000000000000000000, 0.000000000000000000 ) ) ;
#10706=ORIENTED_EDGE ( 'NONE', *, *, #7927, .T. ) ;
#10707=FACE_OUTER_BOUND ( 'NONE', #4293, .T. ) ;
#10712=CARTESIAN_POINT ( 'NONE',  ( 3.346878500200757500, 3.841181488860377247, -6.048595712916176481 ) ) ;
#10720=AXIS2_PLACEMENT_3D ( 'NONE', #5291, #7434, #3366 ) ;
#10723=CARTESIAN_POINT ( 'NONE',  ( 2.500000000000003109, -4.330127018922193649, -6.099999999999999645 ) ) ;
#10740=ORIENTED_EDGE ( 'NONE', *, *, #2304, .T. ) ;
#10748=CARTESIAN_POINT ( 'NONE',  ( 0.000000000000000000, 0.000000000000000000, -4.696360911962001339 ) ) ;
#10751=ORIENTED_EDGE ( 'NONE', *, *, #236, .T. ) ;
#10755=CARTESIAN_POINT ( 'NONE',  ( 2.500000000000000000, 0.000000000000000000, -2.103846626247716234 ) ) ;
#10760=DIRECTION ( 'NONE',  ( -1.000000000000000000, 0.000000000000000000, 0.000000000000000000 ) ) ;
#10763=ORIENTED_EDGE ( 'NONE', *, *, #1253, .F. ) ;
#10768=ORIENTED_EDGE ( 'NONE', *, *, #6551, .F. ) ;
#10769=CARTESIAN_POINT ( 'NONE',  ( -2.500000000000000000, 3.061616997868383141E-16, -6.099999999999999645 ) ) ;
#10775=ORIENTED_EDGE ( 'NONE', *, *, #2024, .T. ) ;
#10779=DIRECTION ( 'NONE',  ( 0.000000000000000000, 0.000000000000000000, -1.000000000000000000 ) ) ;
#10780=CARTESIAN_POINT ( 'NONE',  ( 5.000000000000000000, 2.886751345948134428, -5.653418012614792154 ) ) ;
#10781=FACE_OUTER_BOUND ( 'NONE', #11342, .T. ) ;
#10782=LINE ( 'NONE', #11564, #6152 ) ;
#10786=EDGE_CURVE ( 'NONE', #6890, #1664, #11810, .T. ) ;
#10793=DIRECTION ( 'NONE',  ( 0.8660254037844380415, -0.5000000000000009992, 0.000000000000000000 ) ) ;
#10811=LINE ( 'NONE', #1655, #2374 ) ;
#10820=AXIS2_PLACEMENT_3D ( 'NONE', #11389, #3200, #2063 ) ;
#10838=AXIS2_PLACEMENT_3D ( 'NONE', #5453, #9047, #7371 ) ;
#10841=CARTESIAN_POINT ( 'NONE',  ( 2.500000000000000000, 0.000000000000000000, -0.3755037691048591086 ) ) ;
#10843=VECTOR ( 'NONE', #5994, 1000.000000000000114 ) ;
#10846=EDGE_LOOP ( 'NONE', ( #6013, #7212, #2082, #5475 ) ) ;
#10851=DIRECTION ( 'NONE',  ( 0.000000000000000000, 0.000000000000000000, 1.000000000000000000 ) ) ;
#10853=SHAPE_DEFINITION_REPRESENTATION ( #6920, #9454 ) ;
#10870=CARTESIAN_POINT ( 'NONE',  ( 5.000000000000000888, 0.000000000000000000, -6.099999999999999645 ) ) ;
#10873=CARTESIAN_POINT ( 'NONE',  ( 2.500000000000000000, 0.000000000000000000, -4.696360911962001339 ) ) ;
#10875=EDGE_CURVE ( 'NONE', #10958, #6384, #10663, .T. ) ;
#10881=ORIENTED_EDGE ( 'NONE', *, *, #4904, .T. ) ;
#10889=CARTESIAN_POINT ( 'NONE',  ( 0.000000000000000000, 0.000000000000000000, -3.832189483390572970 ) ) ;
#10902=ADVANCED_FACE ( 'NONE', ( #6413 ), #535, .F. ) ;
#10904=ORIENTED_EDGE ( 'NONE', *, *, #2571, .F. ) ;
#10905=VECTOR ( 'NONE', #2010, 1000.000000000000000 ) ;
#10906=CARTESIAN_POINT ( 'NONE',  ( 0.000000000000000000, 0.000000000000000000, -0.5394676594665810399 ) ) ;
#10909=EDGE_CURVE ( 'NONE', #6890, #7832, #3412, .T. ) ;
#10914=DIRECTION ( 'NONE',  ( -1.000000000000000000, 0.000000000000000000, 0.000000000000000000 ) ) ;
#10933=CARTESIAN_POINT ( 'NONE',  ( 1.648146632868999095, 4.821944789745366222, -6.100000000000003197 ) ) ;
#10935=FACE_OUTER_BOUND ( 'NONE', #6933, .T. ) ;
#10937=VERTEX_POINT ( 'NONE', #8032 ) ;
#10958=VERTEX_POINT ( 'NONE', #7317 ) ;
#10959=DIRECTION ( 'NONE',  ( -0.000000000000000000, -0.000000000000000000, -1.000000000000000000 ) ) ;
#10977=DIRECTION ( 'NONE',  ( -0.000000000000000000, -0.000000000000000000, 1.000000000000000000 ) ) ;
#10987=VERTEX_POINT ( 'NONE', #11237 ) ;
#10991=CIRCLE ( 'NONE', #6427, 2.500000000000000000 ) ;
#10996=CARTESIAN_POINT ( 'NONE',  ( -5.000000000000000888, 0.000000000000000000, 0.000000000000000000 ) ) ;
#11010=CARTESIAN_POINT ( 'NONE',  ( 0.000000000000000000, 0.000000000000000000, -6.099999999999999645 ) ) ;
#11013=CARTESIAN_POINT ( 'NONE',  ( -3.000000000000000888, 0.000000000000000000, -6.074599999999999334 ) ) ;
#11024=EDGE_CURVE ( 'NONE', #3681, #2740, #5121, .T. ) ;
#11027=ORIENTED_EDGE ( 'NONE', *, *, #2950, .F. ) ;
#11030=VERTEX_POINT ( 'NONE', #10996 ) ;
#11035=ORIENTED_EDGE ( 'NONE', *, *, #6539, .F. ) ;
#11037=ADVANCED_FACE ( 'NONE', ( #3705 ), #5693, .F. ) ;
#11045=CARTESIAN_POINT ( 'NONE',  ( -5.000000000000000888, -1.936377641173858466, -0.1973691732449216474 ) ) ;
#11049=B_SPLINE_CURVE_WITH_KNOTS ( 'NONE', 3,
 ( #6137, #1452, #4145, #4209 ),
 .UNSPECIFIED., .F., .F.,
 ( 4, 4 ),
 ( 2.380735200861166196E-07, 0.002921158011986710757 ),
 .UNSPECIFIED. ) ;
#11050=EDGE_LOOP ( 'NONE', ( #1349, #170, #7888, #2691 ) ) ;
#11055=ADVANCED_FACE ( 'NONE', ( #7261 ), #5893, .F. ) ;
#11071=FACE_OUTER_BOUND ( 'NONE', #6503, .T. ) ;
#11078=EDGE_LOOP ( 'NONE', ( #11666, #9222, #45 ) ) ;
#11089=ORIENTED_EDGE ( 'NONE', *, *, #4490, .T. ) ;
#11103=CONICAL_SURFACE ( 'NONE', #9014, 5.000000000000000888, 1.047197551196596299 ) ;
#11107=DIRECTION ( 'NONE',  ( -0.000000000000000000, -0.000000000000000000, -1.000000000000000000 ) ) ;
#11113=CONICAL_SURFACE ( 'NONE', #8078, 3.000000000000000000, 0.9599310885968912466 ) ;
#11119=DIRECTION ( 'NONE',  ( -1.000000000000000000, -1.776356839400250465E-15, 0.000000000000000000 ) ) ;
#11126=ORIENTED_EDGE ( 'NONE', *, *, #1253, .T. ) ;
#11131=ADVANCED_FACE ( 'NONE', ( #6415 ), #9936, .F. ) ;
#11143=CARTESIAN_POINT ( 'NONE',  ( 0.000000000000000000, 0.000000000000000000, -1.239675197676287643 ) ) ;
#11154=DIRECTION ( 'NONE',  ( -0.8660254037844382635, -0.5000000000000005551, 0.000000000000000000 ) ) ;
#11155=DIRECTION ( 'NONE',  ( 0.8191520442889885789, 0.000000000000000000, 0.5735764363510507113 ) ) ;
#11163=CARTESIAN_POINT ( 'NONE',  ( -3.000000000000000000, 3.673940397442059375E-16, 0.000000000000000000 ) ) ;
#11167=DIRECTION ( 'NONE',  ( -1.000000000000000000, 0.000000000000000000, 0.000000000000000000 ) ) ;
#11168=EDGE_CURVE ( 'NONE', #8743, #9107, #5821, .T. ) ;
#11178=CARTESIAN_POINT ( 'NONE',  ( -3.351853367131006234, 3.838309248099017079, 3.542476846806594127E-15 ) ) ;
#11181=STYLED_ITEM ( 'NONE', ( #4280 ), #6721 ) ;
#11191=DIRECTION ( 'NONE',  ( 0.8191520442889885789, 0.000000000000000000, 0.5735764363510507113 ) ) ;
#11193=ADVANCED_FACE ( 'NONE', ( #4792 ), #3195, .F. ) ;
#11194=ORIENTED_EDGE ( 'NONE', *, *, #3680, .T. ) ;
#11204=EDGE_CURVE ( 'NONE', #11822, #1659, #7555, .T. ) ;
#11205=ORIENTED_EDGE ( 'NONE', *, *, #445, .T. ) ;
#11207=AXIS2_PLACEMENT_3D ( 'NONE', #11503, #10428, #2292 ) ;
#11213=CARTESIAN_POINT ( 'NONE',  ( 5.000000000000000888, 0.000000000000000000, 0.000000000000000000 ) ) ;
#11218=VERTEX_POINT ( 'NONE', #8319 ) ;
#11237=CARTESIAN_POINT ( 'NONE',  ( 2.500000000000000000, 0.000000000000000000, -2.103846626247716234 ) ) ;
#11241=EDGE_CURVE ( 'NONE', #5996, #1761, #5698, .T. ) ;
#11247=CARTESIAN_POINT ( 'NONE',  ( 5.000000000000000000, 2.886751345948134428, -0.4465819873852071575 ) ) ;
#11253=CARTESIAN_POINT ( 'NONE',  ( 0.000000000000000000, 0.000000000000000000, -6.099999999999997868 ) ) ;
#11254=B_SPLINE_CURVE_WITH_KNOTS ( 'NONE', 3,
 ( #26, #5495, #10933, #5620 ),
 .UNSPECIFIED., .F., .F.,
 ( 4, 4 ),
 ( 2.380735200817108042E-07, 0.002921158011986720298 ),
 .UNSPECIFIED. ) ;
#11258=VECTOR ( 'NONE', #6650, 1000.000000000000000 ) ;
#11265=CIRCLE ( 'NONE', #8221, 3.000000000000000000 ) ;
#11273=CONICAL_SURFACE ( 'NONE', #6138, 5.000000000000000888, 1.047197551196596299 ) ;
#11274=FACE_OUTER_BOUND ( 'NONE', #6361, .T. ) ;
#11276=( LENGTH_UNIT ( ) NAMED_UNIT ( * ) SI_UNIT ( .MILLI., .METRE. ) );
#11277=FACE_OUTER_BOUND ( 'NONE', #8969, .T. ) ;
#11290=AXIS2_PLACEMENT_3D ( 'NONE', #56, #3724, #1862 ) ;
#11294=LINE ( 'NONE', #11585, #5667 ) ;
#11295=VECTOR ( 'NONE', #227, 1000.000000000000000 ) ;
#11301=ORIENTED_EDGE ( 'NONE', *, *, #8943, .T. ) ;
#11308=EDGE_LOOP ( 'NONE', ( #10029, #1010, #8391, #6217, #3905, #8088 ) ) ;
#11316=CARTESIAN_POINT ( 'NONE',  ( -1.734723475976807094E-14, -5.773502691896260863, -5.653418012614792154 ) ) ;
#11324=DIRECTION ( 'NONE',  ( 0.000000000000000000, 0.000000000000000000, -1.000000000000000000 ) ) ;
#11325=EDGE_CURVE ( 'NONE', #9242, #541, #1690, .T. ) ;
#11336=CARTESIAN_POINT ( 'NONE',  ( 0.000000000000000000, 0.000000000000000000, -2.103846626247716234 ) ) ;
#11340=CARTESIAN_POINT ( 'NONE',  ( -0.8192951148925879945, 5.300482436767278926, -0.1983443223721591819 ) ) ;
#11342=EDGE_LOOP ( 'NONE', ( #3429, #11583, #11126, #9155 ) ) ;
#11348=ADVANCED_FACE ( 'NONE', ( #7612 ), #508, .F. ) ;
#11359=DIRECTION ( 'NONE',  ( 0.000000000000000000, 0.000000000000000000, 1.000000000000000000 ) ) ;
#11377=ORIENTED_EDGE ( 'NONE', *, *, #10548, .F. ) ;
#11383=ORIENTED_EDGE ( 'NONE', *, *, #2510, .T. ) ;
#11385=DIRECTION ( 'NONE',  ( -1.000000000000000000, 0.000000000000000000, 0.000000000000000000 ) ) ;
#11389=CARTESIAN_POINT ( 'NONE',  ( 0.000000000000000000, 0.000000000000000000, -6.099999999999999645 ) ) ;
#11394=EDGE_LOOP ( 'NONE', ( #8332, #3521, #9807 ) ) ;
#11398=CARTESIAN_POINT ( 'NONE',  ( 0.000000000000000000, 5.773502691896260863, -0.4465819873852071575 ) ) ;
#11400=VECTOR ( 'NONE', #2001, 1000.000000000000000 ) ;
#11407=EDGE_CURVE ( 'NONE', #818, #8743, #8560, .T. ) ;
#11418=EDGE_CURVE ( 'NONE', #8673, #8424, #139, .T. ) ;
#11419=ADVANCED_FACE ( 'NONE', ( #1221 ), #5672, .T. ) ;
#11424=CIRCLE ( 'NONE', #6100, 3.000000000000000888 ) ;
#11430=CARTESIAN_POINT ( 'NONE',  ( 3.000000000000000000, 3.673940397442059868E-16, -5.210428571428570521 ) ) ;
#11435=FACE_OUTER_BOUND ( 'NONE', #4718, .T. ) ;
#11453=ORIENTED_EDGE ( 'NONE', *, *, #8075, .T. ) ;
#11455=ADVANCED_FACE ( 'NONE', ( #1163 ), #3969, .T. ) ;
#11465=CARTESIAN_POINT ( 'NONE',  ( -3.000000000000000000, 0.000000000000000000, -2.617914285714285416 ) ) ;
#11471=AXIS2_PLACEMENT_3D ( 'NONE', #7879, #184, #9235 ) ;
#11477=AXIS2_PLACEMENT_3D ( 'NONE', #1786, #5511, #7260 ) ;
#11483=VECTOR ( 'NONE', #8997, 1000.000000000000000 ) ;
#11490=EDGE_LOOP ( 'NONE', ( #5354, #7569, #6998, #947 ) ) ;
#11491=CARTESIAN_POINT ( 'NONE',  ( 2.500000000000005773, 4.330127018922190985, -6.099999999999999645 ) ) ;
#11493=VECTOR ( 'NONE', #1036, 1000.000000000000000 ) ;
#11495=ORIENTED_EDGE ( 'NONE', *, *, #1903, .T. ) ;
#11503=CARTESIAN_POINT ( 'NONE',  ( 0.000000000000000000, 0.000000000000000000, -6.099999999999999645 ) ) ;
#11507=EDGE_LOOP ( 'NONE', ( #4680, #3601, #4873, #4370 ) ) ;
#11510=CARTESIAN_POINT ( 'NONE',  ( 0.000000000000000000, 0.000000000000000000, -0.8895714285714284575 ) ) ;
#11516=CARTESIAN_POINT ( 'NONE',  ( -2.925285743277529438, -4.084588180558409221, -0.01055556052339341917 ) ) ;
#11519=VERTEX_POINT ( 'NONE', #1409 ) ;
#11530=ORIENTED_EDGE ( 'NONE', *, *, #11418, .F. ) ;
#11534=CARTESIAN_POINT ( 'NONE',  ( 2.500000000000003109, -4.330127018922193649, 0.000000000000000000 ) ) ;
#11543=ORIENTED_EDGE ( 'NONE', *, *, #6770, .F. ) ;
#11550=CARTESIAN_POINT ( 'NONE',  ( 4.999999999999998224, -2.886751345948137981, -0.4465819873852071575 ) ) ;
#11553=ORIENTED_EDGE ( 'NONE', *, *, #8805, .F. ) ;
#11554=DIRECTION ( 'NONE',  ( 0.000000000000000000, 0.000000000000000000, 1.000000000000000000 ) ) ;
#11558=DIRECTION ( 'NONE',  ( -0.000000000000000000, -0.000000000000000000, -1.000000000000000000 ) ) ;
#11564=CARTESIAN_POINT ( 'NONE',  ( -2.500000000000000000, 3.061616997868383141E-16, -6.099999999999999645 ) ) ;
#11565=ORIENTED_EDGE ( 'NONE', *, *, #10157, .T. ) ;
#11567=DIRECTION ( 'NONE',  ( 0.000000000000000000, 0.000000000000000000, -1.000000000000000000 ) ) ;
#11571=FACE_OUTER_BOUND ( 'NONE', #1634, .T. ) ;
#11572=SURFACE_SIDE_STYLE ('',( #2542 ) ) ;
#11573=DIRECTION ( 'NONE',  ( -1.000000000000000000, 0.000000000000000000, 0.000000000000000000 ) ) ;
#11578=ORIENTED_EDGE ( 'NONE', *, *, #1308, .T. ) ;
#11583=ORIENTED_EDGE ( 'NONE', *, *, #453, .T. ) ;
#11585=CARTESIAN_POINT ( 'NONE',  ( 3.000000000000000000, 3.673940397442059868E-16, -2.617914285714285416 ) ) ;
#11590=ORIENTED_EDGE ( 'NONE', *, *, #1610, .T. ) ;
#11594=CARTESIAN_POINT ( 'NONE',  ( 0.000000000000000000, 0.000000000000000000, -5.210428571428570521 ) ) ;
#11595=CARTESIAN_POINT ( 'NONE',  ( -2.500000000000005773, -4.330127018922191873, 0.000000000000000000 ) ) ;
#11608=EDGE_CURVE ( 'NONE', #1322, #9858, #1265, .T. ) ;
#11611=CARTESIAN_POINT ( 'NONE',  ( 2.712167343862819990, 4.207632145829745873, -6.100000000000002309 ) ) ;
#11620=FACE_OUTER_BOUND ( 'NONE', #6391, .T. ) ;
#11626=ORIENTED_EDGE ( 'NONE', *, *, #11204, .T. ) ;
#11629=DIRECTION ( 'NONE',  ( -0.000000000000000000, -0.000000000000000000, -1.000000000000000000 ) ) ;
#11636=CARTESIAN_POINT ( 'NONE',  ( 3.556264818047235376, 3.720292241887087847, -0.08165819712376884421 ) ) ;
#11640=AXIS2_PLACEMENT_3D ( 'NONE', #1720, #10634, #4428 ) ;
#11642=ORIENTED_EDGE ( 'NONE', *, *, #8074, .F. ) ;
#11648=EDGE_LOOP ( 'NONE', ( #5590, #2930, #9114, #8894 ) ) ;
#11650=AXIS2_PLACEMENT_3D ( 'NONE', #10889, #3594, #8318 ) ;
#11653=AXIS2_PLACEMENT_3D ( 'NONE', #825, #4497, #1907 ) ;
#11657=CARTESIAN_POINT ( 'NONE',  ( 5.000000000000000000, 2.886751345948124214, -6.099999999999999645 ) ) ;
#11662=CARTESIAN_POINT ( 'NONE',  ( 0.000000000000000000, 0.000000000000000000, -25.03750572909317285 ) ) ;
#11666=ORIENTED_EDGE ( 'NONE', *, *, #8514, .T. ) ;
#11667=FACE_OUTER_BOUND ( 'NONE', #740, .T. ) ;
#11671=CIRCLE ( 'NONE', #11477, 5.000000000000000888 ) ;
#11674=DIRECTION ( 'NONE',  ( -1.000000000000000000, 0.000000000000000000, 0.000000000000000000 ) ) ;
#11676=CARTESIAN_POINT ( 'NONE',  ( 2.500000000000000000, 0.000000000000000000, -6.099999999999999645 ) ) ;
#11682=DIRECTION ( 'NONE',  ( 0.000000000000000000, 0.000000000000000000, 1.000000000000000000 ) ) ;
#11686=AXIS2_PLACEMENT_3D ( 'NONE', #6850, #2520, #9817 ) ;
#11688=ORIENTED_EDGE ( 'NONE', *, *, #11608, .T. ) ;
#11694=VECTOR ( 'NONE', #2628, 1000.000000000000000 ) ;
#11703=CARTESIAN_POINT ( 'NONE',  ( 5.000000000000000000, 2.886751345948134428, -0.4465819873852071575 ) ) ;
#11704=ORIENTED_EDGE ( 'NONE', *, *, #1610, .F. ) ;
#11707=EDGE_LOOP ( 'NONE', ( #10158, #3639, #8411, #10511 ) ) ;
#11717=PLANE ( 'NONE',  #8693 ) ;
#11728=DIRECTION ( 'NONE',  ( 1.000000000000000000, 0.000000000000000000, 0.000000000000000000 ) ) ;
#11729=ADVANCED_FACE ( 'NONE', ( #5305 ), #331, .F. ) ;
#11733=DIRECTION ( 'NONE',  ( 0.000000000000000000, 0.000000000000000000, 1.000000000000000000 ) ) ;
#11745=ORIENTED_EDGE ( 'NONE', *, *, #8926, .T. ) ;
#11748=CARTESIAN_POINT ( 'NONE',  ( 0.000000000000000000, 0.000000000000000000, -0.3851141460153411078 ) ) ;
#11753=CARTESIAN_POINT ( 'NONE',  ( 2.500000000000005773, 4.330127018922190985, 0.000000000000000000 ) ) ;
#11772=CARTESIAN_POINT ( 'NONE',  ( -3.346878500200761053, -3.841181488860384796, -6.048595712916170264 ) ) ;
#11778=ADVANCED_FACE ( 'NONE', ( #6383 ), #3502, .T. ) ;
#11784=DIRECTION ( 'NONE',  ( -1.000000000000000000, 0.000000000000000000, 0.000000000000000000 ) ) ;
#11795=EDGE_LOOP ( 'NONE', ( #2816, #1232, #7647 ) ) ;
#11800=CARTESIAN_POINT ( 'NONE',  ( -3.000000000000000888, 0.000000000000000000, -6.074599999999999334 ) ) ;
#11804=EDGE_LOOP ( 'NONE', ( #2427, #4488, #3254, #5152, #2221, #10628 ) ) ;
#11810=CIRCLE ( 'NONE', #8188, 2.500000000000000000 ) ;
#11814=CARTESIAN_POINT ( 'NONE',  ( 3.346878500200757056, 3.841181488860378135, -0.05140428708382578649 ) ) ;
#11815=ORIENTED_EDGE ( 'NONE', *, *, #7328, .F. ) ;
#11822=VERTEX_POINT ( 'NONE', #6549 ) ;
#11828=CARTESIAN_POINT ( 'NONE',  ( 5.000000000000000000, -0.4878135028931874784, 5.353248226647178143E-16 ) ) ;
#11829=DIRECTION ( 'NONE',  ( 0.000000000000000000, 0.000000000000000000, -1.000000000000000000 ) ) ;
#11832=CARTESIAN_POINT ( 'NONE',  ( 0.000000000000000000, 0.000000000000000000, -2.617914285714285416 ) ) ;
#11839=VERTEX_POINT ( 'NONE', #11247 ) ;
#11841=CARTESIAN_POINT ( 'NONE',  ( 0.000000000000000000, 0.000000000000000000, -6.099999999999999645 ) ) ;
#11848=ORIENTED_EDGE ( 'NONE', *, *, #4153, .T. ) ;
#11889=COLOUR_RGB('Black',0.12,0.14,0.17);
#11890=FILL_AREA_STYLE_COLOUR('',#11889);
#11891=FILL_AREA_STYLE('',(#11890));
#11892=SURFACE_STYLE_FILL_AREA(#11891);
#11893=SURFACE_SIDE_STYLE('',(#11892));
#11894=SURFACE_STYLE_USAGE(.BOTH.,#11893);
#11895=PRESENTATION_STYLE_ASSIGNMENT((#11894));
ENDSEC;
END-ISO-10303-21;
